ISO-10303-21;
HEADER;
FILE_DESCRIPTION (('STEP AP214'),
    '1' );
FILE_NAME ('bottom housing_bottom housing.step',
    '2026-10-08T15:02:10',
    ( '' ),
    ( '' ),
    'SwSTEP 2.0',
    'SolidWorks 2026',
    '' );
FILE_SCHEMA (( 'AUTOMOTIVE_DESIGN' ));
ENDSEC;

DATA;
#11=VERTEX_POINT ( 'NONE', #9296 ) ;
#23=ORIENTED_EDGE ( 'NONE', *, *, #2267, .F. ) ;
#32=DIRECTION ( 'NONE',  ( -1.000000000000000000, 0.000000000000000000, 0.000000000000000000 ) ) ;
#65=EDGE_CURVE ( 'NONE', #2304, #13811, #1543, .T. ) ;
#68=VERTEX_POINT ( 'NONE', #19405 ) ;
#72=CARTESIAN_POINT ( 'NONE',  ( 0.000000000000000000, 24.63401512838747820, -77.51594804401857175 ) ) ;
#73=VECTOR ( 'NONE', #4649, 1000.000000000000000 ) ;
#82=CIRCLE ( 'NONE', #20492, 19.79999999999999716 ) ;
#152=AXIS2_PLACEMENT_3D ( 'NONE', #2857, #13336, #13120 ) ;
#164=ORIENTED_EDGE ( 'NONE', *, *, #3485, .T. ) ;
#208=CIRCLE ( 'NONE', #12782, 23.00000000000000000 ) ;
#211=CIRCLE ( 'NONE', #21742, 17.50000000000000711 ) ;
#215=VERTEX_POINT ( 'NONE', #16158 ) ;
#227=DIRECTION ( 'NONE',  ( -1.000000000000000000, 0.000000000000000000, -0.000000000000000000 ) ) ;
#231=DIRECTION ( 'NONE',  ( -2.162300680179923768E-16, -1.000000000000000000, 0.000000000000000000 ) ) ;
#245=CARTESIAN_POINT ( 'NONE',  ( -23.00000000000000000, 0.000000000000000000, 75.00000000000000000 ) ) ;
#292=ORIENTED_EDGE ( 'NONE', *, *, #18240, .F. ) ;
#297=DIRECTION ( 'NONE',  ( 0.000000000000000000, 0.000000000000000000, 1.000000000000000000 ) ) ;
#310=DIRECTION ( 'NONE',  ( -6.982962677686266711E-15, 1.000000000000000000, 0.000000000000000000 ) ) ;
#331=EDGE_LOOP ( 'NONE', ( #8318, #981, #21331, #9100 ) ) ;
#357=EDGE_CURVE ( 'NONE', #14271, #20366, #5815, .T. ) ;
#359=CARTESIAN_POINT ( 'NONE',  ( 0.000000000000000000, 19.63401512838747820, 77.51594804401857175 ) ) ;
#371=CARTESIAN_POINT ( 'NONE',  ( 0.000000000000000000, -17.50000000000000711, -30.00000000000000000 ) ) ;
#399=ORIENTED_EDGE ( 'NONE', *, *, #20384, .T. ) ;
#417=CARTESIAN_POINT ( 'NONE',  ( 0.000000000000000000, 25.00000000000000000, 75.00000000000000000 ) ) ;
#435=ORIENTED_EDGE ( 'NONE', *, *, #10221, .T. ) ;
#444=FACE_OUTER_BOUND ( 'NONE', #12908, .T. ) ;
#447=CARTESIAN_POINT ( 'NONE',  ( 1.526556658859590243E-13, -22.63401512838748175, -77.51594804401857175 ) ) ;
#454=ORIENTED_EDGE ( 'NONE', *, *, #861, .T. ) ;
#456=ORIENTED_EDGE ( 'NONE', *, *, #16713, .T. ) ;
#458=CIRCLE ( 'NONE', #800, 23.00000000000000000 ) ;
#463=CARTESIAN_POINT ( 'NONE',  ( 1.526556658859590243E-13, -22.63401512838748175, 77.51594804401857175 ) ) ;
#464=EDGE_CURVE ( 'NONE', #19761, #19544, #19810, .T. ) ;
#471=AXIS2_PLACEMENT_3D ( 'NONE', #20639, #5224, #4585 ) ;
#473=EDGE_CURVE ( 'NONE', #16430, #17437, #6541, .T. ) ;
#487=AXIS2_PLACEMENT_3D ( 'NONE', #4624, #8133, #8020 ) ;
#488=CIRCLE ( 'NONE', #9121, 3.000000000000002665 ) ;
#516=ORIENTED_EDGE ( 'NONE', *, *, #704, .F. ) ;
#522=AXIS2_PLACEMENT_3D ( 'NONE', #21767, #13572, #13228 ) ;
#550=EDGE_CURVE ( 'NONE', #16938, #19932, #17685, .T. ) ;
#553=AXIS2_PLACEMENT_3D ( 'NONE', #16638, #4473, #5947 ) ;
#557=DIRECTION ( 'NONE',  ( 0.000000000000000000, 0.000000000000000000, -1.000000000000000000 ) ) ;
#558=DIRECTION ( 'NONE',  ( -0.000000000000000000, -1.000000000000000000, -0.000000000000000000 ) ) ;
#586=EDGE_CURVE ( 'NONE', #10093, #20645, #8701, .T. ) ;
#595=DIRECTION ( 'NONE',  ( 0.000000000000000000, 0.000000000000000000, 1.000000000000000000 ) ) ;
#613=CARTESIAN_POINT ( 'NONE',  ( -19.79999999999999716, 0.000000000000000000, -78.50000000000000000 ) ) ;
#622=FACE_OUTER_BOUND ( 'NONE', #10894, .T. ) ;
#642=CARTESIAN_POINT ( 'NONE',  ( 0.000000000000000000, 17.50000000000000711, -60.00000000000000000 ) ) ;
#671=ORIENTED_EDGE ( 'NONE', *, *, #17680, .T. ) ;
#675=ADVANCED_FACE ( 'NONE', ( #14692 ), #2927, .F. ) ;
#704=EDGE_CURVE ( 'NONE', #20426, #16938, #13106, .T. ) ;
#728=ORIENTED_EDGE ( 'NONE', *, *, #22146, .F. ) ;
#739=PLANE ( 'NONE',  #21317 ) ;
#740=LINE ( 'NONE', #2534, #17773 ) ;
#761=CARTESIAN_POINT ( 'NONE',  ( 0.000000000000000000, -23.00000000000000000, -24.99999999999999645 ) ) ;
#767=DIRECTION ( 'NONE',  ( -0.000000000000000000, -1.000000000000000000, -0.000000000000000000 ) ) ;
#785=CARTESIAN_POINT ( 'NONE',  ( 0.000000000000000000, 25.00000000000000000, -75.00000000000000000 ) ) ;
#787=ADVANCED_FACE ( 'NONE', ( #3181 ), #2218, .F. ) ;
#800=AXIS2_PLACEMENT_3D ( 'NONE', #3925, #7323, #14193 ) ;
#802=CARTESIAN_POINT ( 'NONE',  ( 0.000000000000000000, -23.00000000000000000, -30.00000000000000000 ) ) ;
#814=VECTOR ( 'NONE', #17946, 1000.000000000000000 ) ;
#861=EDGE_CURVE ( 'NONE', #21809, #17987, #12650, .T. ) ;
#862=VERTEX_POINT ( 'NONE', #359 ) ;
#880=CARTESIAN_POINT ( 'NONE',  ( 0.000000000000000000, 0.000000000000000000, -60.00000000000001421 ) ) ;
#900=CYLINDRICAL_SURFACE ( 'NONE', #10131, 17.50000000000000711 ) ;
#901=CIRCLE ( 'NONE', #21740, 3.000000000000002665 ) ;
#920=VECTOR ( 'NONE', #9719, 1000.000000000000000 ) ;
#955=EDGE_CURVE ( 'NONE', #17437, #15809, #17323, .T. ) ;
#961=EDGE_LOOP ( 'NONE', ( #6548, #6973, #3988, #4970 ) ) ;
#981=ORIENTED_EDGE ( 'NONE', *, *, #19244, .F. ) ;
#997=CARTESIAN_POINT ( 'NONE',  ( 0.000000000000000000, 0.000000000000000000, -78.50000000000000000 ) ) ;
#1019=ORIENTED_EDGE ( 'NONE', *, *, #7643, .T. ) ;
#1079=DIRECTION ( 'NONE',  ( -0.000000000000000000, -0.000000000000000000, -1.000000000000000000 ) ) ;
#1091=DIRECTION ( 'NONE',  ( -1.000000000000000000, 0.000000000000000000, 0.000000000000000000 ) ) ;
#1126=CARTESIAN_POINT ( 'NONE',  ( 1.665334536937734811E-13, -24.63401512838747820, 77.51594804401857175 ) ) ;
#1141=EDGE_CURVE ( 'NONE', #12646, #6063, #20818, .T. ) ;
#1144=CARTESIAN_POINT ( 'NONE',  ( 1.665334536937734811E-13, -23.00000000000000000, 69.99999999999998579 ) ) ;
#1152=VERTEX_POINT ( 'NONE', #20394 ) ;
#1171=AXIS2_PLACEMENT_3D ( 'NONE', #5653, #12637, #8934 ) ;
#1173=AXIS2_PLACEMENT_3D ( 'NONE', #1126, #16330, #2912 ) ;
#1184=CARTESIAN_POINT ( 'NONE',  ( 1.526556658859590243E-13, -21.80000000000000071, 78.50000000000000000 ) ) ;
#1196=EDGE_LOOP ( 'NONE', ( #14058, #1375, #16150, #10148 ) ) ;
#1201=DIRECTION ( 'NONE',  ( 0.000000000000000000, 0.000000000000000000, -1.000000000000000000 ) ) ;
#1205=CARTESIAN_POINT ( 'NONE',  ( 0.000000000000000000, 0.000000000000000000, 75.00000000000000000 ) ) ;
#1208=CIRCLE ( 'NONE', #18833, 3.000000000000002665 ) ;
#1220=DIRECTION ( 'NONE',  ( -1.000000000000000000, 0.000000000000000000, 0.000000000000000000 ) ) ;
#1237=EDGE_CURVE ( 'NONE', #12803, #17859, #13371, .T. ) ;
#1313=CARTESIAN_POINT ( 'NONE',  ( 0.000000000000000000, 23.00000000000000000, -69.99999999999998579 ) ) ;
#1314=EDGE_LOOP ( 'NONE', ( #1892, #17605, #13463, #18308 ) ) ;
#1332=CARTESIAN_POINT ( 'NONE',  ( -19.63401512838747820, 0.000000000000000000, 77.51594804401857175 ) ) ;
#1336=ORIENTED_EDGE ( 'NONE', *, *, #14070, .F. ) ;
#1343=EDGE_LOOP ( 'NONE', ( #18591, #20601, #5350, #21894 ) ) ;
#1355=LINE ( 'NONE', #3251, #13869 ) ;
#1375=ORIENTED_EDGE ( 'NONE', *, *, #1141, .T. ) ;
#1377=AXIS2_PLACEMENT_3D ( 'NONE', #15606, #297, #5573 ) ;
#1392=DIRECTION ( 'NONE',  ( 0.000000000000000000, 0.000000000000000000, -1.000000000000000000 ) ) ;
#1406=CARTESIAN_POINT ( 'NONE',  ( 0.000000000000000000, -25.00000000000000000, 75.00000000000000000 ) ) ;
#1421=CARTESIAN_POINT ( 'NONE',  ( -17.50000000000000711, 0.000000000000000000, -24.99999999999999645 ) ) ;
#1444=ADVANCED_FACE ( 'NONE', ( #13058 ), #900, .F. ) ;
#1503=DIRECTION ( 'NONE',  ( -0.000000000000000000, -0.000000000000000000, -1.000000000000000000 ) ) ;
#1529=CIRCLE ( 'NONE', #7295, 20.99999999999999645 ) ;
#1535=ORIENTED_EDGE ( 'NONE', *, *, #21161, .T. ) ;
#1543=CIRCLE ( 'NONE', #9800, 25.00000000000000000 ) ;
#1551=CARTESIAN_POINT ( 'NONE',  ( 0.000000000000000000, 0.000000000000000000, -55.00000000000000000 ) ) ;
#1554=ADVANCED_FACE ( 'NONE', ( #18239 ), #2363, .T. ) ;
#1560=EDGE_LOOP ( 'NONE', ( #10535, #10990, #6034, #13613, #17716, #18477 ) ) ;
#1564=VERTEX_POINT ( 'NONE', #6072 ) ;
#1570=AXIS2_PLACEMENT_3D ( 'NONE', #16970, #6954, #8425 ) ;
#1573=EDGE_CURVE ( 'NONE', #2436, #16180, #2800, .T. ) ;
#1604=VERTEX_POINT ( 'NONE', #785 ) ;
#1612=CARTESIAN_POINT ( 'NONE',  ( 0.000000000000000000, 23.00000000000000000, 75.00000000000000000 ) ) ;
#1627=AXIS2_PLACEMENT_3D ( 'NONE', #997, #7872, #9772 ) ;
#1650=DIRECTION ( 'NONE',  ( 0.000000000000000000, 0.000000000000000000, -1.000000000000000000 ) ) ;
#1651=ORIENTED_EDGE ( 'NONE', *, *, #15761, .F. ) ;
#1662=LINE ( 'NONE', #17085, #13418 ) ;
#1692=CARTESIAN_POINT ( 'NONE',  ( 1.387778780781445676E-13, -19.79999999999999716, -78.50000000000000000 ) ) ;
#1694=PRODUCT_DEFINITION_SHAPE ( 'NONE', 'NONE',  #7130 ) ;
#1757=DIRECTION ( 'NONE',  ( -1.000000000000000000, 0.000000000000000000, 0.000000000000000000 ) ) ;
#1768=CARTESIAN_POINT ( 'NONE',  ( 1.317067778529001989E-13, -19.63401512838747820, 77.51594804401857175 ) ) ;
#1783=ORIENTED_EDGE ( 'NONE', *, *, #21371, .T. ) ;
#1807=CARTESIAN_POINT ( 'NONE',  ( 0.000000000000000000, 17.50000000000000711, -24.99999999999999645 ) ) ;
#1822=FILL_AREA_STYLE ('',( #18935 ) ) ;
#1829=FACE_OUTER_BOUND ( 'NONE', #331, .T. ) ;
#1845=LINE ( 'NONE', #7151, #18501 ) ;
#1856=CIRCLE ( 'NONE', #6174, 23.00000000000000000 ) ;
#1862=EDGE_LOOP ( 'NONE', ( #17430, #6696, #13469, #7808 ) ) ;
#1865=CARTESIAN_POINT ( 'NONE',  ( 0.000000000000000000, 0.000000000000000000, -55.00000000000000000 ) ) ;
#1873=CARTESIAN_POINT ( 'NONE',  ( -22.63401512838748175, 0.000000000000000000, 77.51594804401857175 ) ) ;
#1878=CIRCLE ( 'NONE', #14472, 3.000000000000002665 ) ;
#1885=ORIENTED_EDGE ( 'NONE', *, *, #955, .T. ) ;
#1891=DIRECTION ( 'NONE',  ( -0.000000000000000000, -0.000000000000000000, -1.000000000000000000 ) ) ;
#1892=ORIENTED_EDGE ( 'NONE', *, *, #12725, .F. ) ;
#1899=AXIS2_PLACEMENT_3D ( 'NONE', #17393, #8729, #17277 ) ;
#1905=DIRECTION ( 'NONE',  ( -1.000000000000000000, -6.982962677686266711E-15, 0.000000000000000000 ) ) ;
#1956=VERTEX_POINT ( 'NONE', #18892 ) ;
#1960=CARTESIAN_POINT ( 'NONE',  ( 0.000000000000000000, 0.000000000000000000, -75.00000000000000000 ) ) ;
#1985=ORIENTED_EDGE ( 'NONE', *, *, #15578, .T. ) ;
#1988=CARTESIAN_POINT ( 'NONE',  ( 0.000000000000000000, 21.00000000000000000, 75.00000000000000000 ) ) ;
#2011=CIRCLE ( 'NONE', #21053, 21.80000000000000071 ) ;
#2056=LINE ( 'NONE', #5422, #9459 ) ;
#2110=ORIENTED_EDGE ( 'NONE', *, *, #15578, .F. ) ;
#2129=DIRECTION ( 'NONE',  ( -0.000000000000000000, -0.000000000000000000, -1.000000000000000000 ) ) ;
#2181=DIRECTION ( 'NONE',  ( -0.000000000000000000, -0.000000000000000000, -1.000000000000000000 ) ) ;
#2185=ORIENTED_EDGE ( 'NONE', *, *, #9624, .T. ) ;
#2203=DIRECTION ( 'NONE',  ( -0.000000000000000000, -0.000000000000000000, 1.000000000000000000 ) ) ;
#2207=CARTESIAN_POINT ( 'NONE',  ( 1.387778780781445676E-13, -19.79999999999999716, -78.50000000000000000 ) ) ;
#2218=TOROIDAL_SURFACE ( 'NONE', #7979, 24.63401512838747820, 3.000000000000000888 ) ;
#2219=ORIENTED_EDGE ( 'NONE', *, *, #4940, .T. ) ;
#2221=DIRECTION ( 'NONE',  ( -1.000000000000000000, 0.000000000000000000, 0.000000000000000000 ) ) ;
#2227=UNCERTAINTY_MEASURE_WITH_UNIT (LENGTH_MEASURE( 1.000000000000000082E-05 ), #7286, 'distance_accuracy_value', 'NONE');
#2233=PLANE ( 'NONE',  #13796 ) ;
#2239=EDGE_CURVE ( 'NONE', #17987, #10013, #9076, .T. ) ;
#2247=CIRCLE ( 'NONE', #20205, 3.000000000000002665 ) ;
#2267=EDGE_CURVE ( 'NONE', #4321, #7303, #16977, .T. ) ;
#2304=VERTEX_POINT ( 'NONE', #19331 ) ;
#2315=CARTESIAN_POINT ( 'NONE',  ( 0.000000000000000000, 0.000000000000000000, -77.51594804401857175 ) ) ;
#2321=EDGE_CURVE ( 'NONE', #19351, #20853, #6917, .T. ) ;
#2333=DIRECTION ( 'NONE',  ( 1.000000000000000000, 0.000000000000000000, 0.000000000000000000 ) ) ;
#2344=VECTOR ( 'NONE', #17003, 1000.000000000000000 ) ;
#2346=AXIS2_PLACEMENT_3D ( 'NONE', #19041, #4979, #6679 ) ;
#2348=CARTESIAN_POINT ( 'NONE',  ( 0.000000000000000000, 0.000000000000000000, -60.00000000000000000 ) ) ;
#2355=VERTEX_POINT ( 'NONE', #5486 ) ;
#2363=PLANE ( 'NONE',  #18045 ) ;
#2365=VECTOR ( 'NONE', #21604, 1000.000000000000000 ) ;
#2395=EDGE_CURVE ( 'NONE', #21209, #22159, #3546, .T. ) ;
#2396=CARTESIAN_POINT ( 'NONE',  ( 0.000000000000000000, 20.99999999999999645, -69.99999999999998579 ) ) ;
#2436=VERTEX_POINT ( 'NONE', #8887 ) ;
#2442=CARTESIAN_POINT ( 'NONE',  ( 0.000000000000000000, 21.80000000000000071, -78.50000000000000000 ) ) ;
#2463=ORIENTED_EDGE ( 'NONE', *, *, #3719, .F. ) ;
#2472=CARTESIAN_POINT ( 'NONE',  ( 0.000000000000000000, 0.000000000000000000, 75.00000000000000000 ) ) ;
#2499=ADVANCED_FACE ( 'NONE', ( #17315 ), #19432, .F. ) ;
#2500=EDGE_LOOP ( 'NONE', ( #6718, #14451, #20486, #19386, #1651, #7087, #8905, #5065, #16599, #16028, #3097, #14085, #3262, #8443, #4239, #18996, #11919, #12097, #16271, #17566, #1885, #456, #13925, #4784, #8626, #14159 ) ) ;
#2521=CARTESIAN_POINT ( 'NONE',  ( -17.50000000000000711, 0.000000000000000000, -30.00000000000000000 ) ) ;
#2522=ORIENTED_EDGE ( 'NONE', *, *, #21445, .F. ) ;
#2533=CARTESIAN_POINT ( 'NONE',  ( 0.000000000000000000, 0.000000000000000000, 69.99999999999998579 ) ) ;
#2534=CARTESIAN_POINT ( 'NONE',  ( -20.99999999999999645, 0.000000000000000000, 60.00000000000001421 ) ) ;
#2563=DIRECTION ( 'NONE',  ( -4.408728476930466911E-15, 1.000000000000000000, 0.000000000000000000 ) ) ;
#2564=AXIS2_PLACEMENT_3D ( 'NONE', #463, #15664, #8383 ) ;
#2573=ORIENTED_EDGE ( 'NONE', *, *, #12275, .T. ) ;
#2576=AXIS2_PLACEMENT_3D ( 'NONE', #12006, #18973, #14370 ) ;
#2596=EDGE_CURVE ( 'NONE', #10013, #21551, #17214, .T. ) ;
#2626=VECTOR ( 'NONE', #310, 1000.000000000000000 ) ;
#2632=CARTESIAN_POINT ( 'NONE',  ( 0.000000000000000000, 0.000000000000000000, -75.00000000000000000 ) ) ;
#2640=AXIS2_PLACEMENT_3D ( 'NONE', #13593, #20431, #14833 ) ;
#2671=CARTESIAN_POINT ( 'NONE',  ( -17.50000000000000711, 0.000000000000000000, -24.99999999999999645 ) ) ;
#2686=ORIENTED_EDGE ( 'NONE', *, *, #3303, .F. ) ;
#2694=VECTOR ( 'NONE', #13370, 1000.000000000000000 ) ;
#2707=DIRECTION ( 'NONE',  ( 1.000000000000000000, 0.000000000000000000, 0.000000000000000000 ) ) ;
#2715=CYLINDRICAL_SURFACE ( 'NONE', #487, 25.00000000000000000 ) ;
#2722=ORIENTED_EDGE ( 'NONE', *, *, #15991, .T. ) ;
#2731=CARTESIAN_POINT ( 'NONE',  ( 0.000000000000000000, 0.000000000000000000, -55.00000000000000000 ) ) ;
#2741=CARTESIAN_POINT ( 'NONE',  ( 1.526556658859590243E-13, -22.63401512838748175, 77.51594804401857175 ) ) ;
#2779=CARTESIAN_POINT ( 'NONE',  ( 0.000000000000000000, 0.000000000000000000, 75.00000000000000000 ) ) ;
#2800=LINE ( 'NONE', #11256, #21622 ) ;
#2809=ORIENTED_EDGE ( 'NONE', *, *, #5897, .F. ) ;
#2824=PLANE ( 'NONE',  #5505 ) ;
#2845=DIRECTION ( 'NONE',  ( -0.000000000000000000, -0.000000000000000000, -1.000000000000000000 ) ) ;
#2857=CARTESIAN_POINT ( 'NONE',  ( 0.000000000000000000, 0.000000000000000000, 78.50000000000000000 ) ) ;
#2873=CARTESIAN_POINT ( 'NONE',  ( 0.000000000000000000, 0.000000000000000000, -77.51594804401857175 ) ) ;
#2879=DIRECTION ( 'NONE',  ( 0.000000000000000000, 0.000000000000000000, 1.000000000000000000 ) ) ;
#2912=DIRECTION ( 'NONE',  ( 0.000000000000000000, 0.000000000000000000, 1.000000000000000000 ) ) ;
#2918=DIRECTION ( 'NONE',  ( -1.000000000000000000, 0.000000000000000000, 0.000000000000000000 ) ) ;
#2927=TOROIDAL_SURFACE ( 'NONE', #15887, 24.63401512838747820, 3.000000000000000888 ) ;
#2928=CARTESIAN_POINT ( 'NONE',  ( -23.00000000000000355, 0.000000000000000000, 75.00000000000000000 ) ) ;
#2937=VERTEX_POINT ( 'NONE', #2442 ) ;
#2969=CARTESIAN_POINT ( 'NONE',  ( 0.000000000000000000, 17.50000000000000711, -55.00000000000000000 ) ) ;
#2973=AXIS2_PLACEMENT_3D ( 'NONE', #4346, #8804, #6153 ) ;
#2974=DIRECTION ( 'NONE',  ( 0.000000000000000000, 0.000000000000000000, 1.000000000000000000 ) ) ;
#2993=AXIS2_PLACEMENT_3D ( 'NONE', #7756, #767, #11236 ) ;
#3005=FACE_OUTER_BOUND ( 'NONE', #8881, .T. ) ;
#3025=AXIS2_PLACEMENT_3D ( 'NONE', #12759, #20022, #17720 ) ;
#3029=CARTESIAN_POINT ( 'NONE',  ( 0.000000000000000000, 24.63401512838747820, -77.51594804401857175 ) ) ;
#3030=CARTESIAN_POINT ( 'NONE',  ( 1.665334536937734811E-13, -23.00000000000000000, 69.99999999999998579 ) ) ;
#3043=TOROIDAL_SURFACE ( 'NONE', #553, 24.63401512838747820, 3.000000000000000888 ) ;
#3051=EDGE_LOOP ( 'NONE', ( #12162, #17052, #20195, #14283 ) ) ;
#3056=TOROIDAL_SURFACE ( 'NONE', #8439, 24.63401512838747820, 3.000000000000000888 ) ;
#3069=CARTESIAN_POINT ( 'NONE',  ( 0.000000000000000000, 0.000000000000000000, -24.99999999999999645 ) ) ;
#3078=EDGE_CURVE ( 'NONE', #16621, #14271, #12179, .T. ) ;
#3097=ORIENTED_EDGE ( 'NONE', *, *, #16505, .F. ) ;
#3106=CARTESIAN_POINT ( 'NONE',  ( 0.000000000000000000, 0.000000000000000000, -75.00000000000000000 ) ) ;
#3122=LINE ( 'NONE', #18556, #2694 ) ;
#3143=LINE ( 'NONE', #4947, #2344 ) ;
#3181=FACE_OUTER_BOUND ( 'NONE', #7005, .T. ) ;
#3205=VERTEX_POINT ( 'NONE', #16292 ) ;
#3224=DIRECTION ( 'NONE',  ( -1.000000000000000000, 0.000000000000000000, 0.000000000000000000 ) ) ;
#3251=CARTESIAN_POINT ( 'NONE',  ( 1.665334536937734811E-13, -23.00000000000000000, -69.99999999999998579 ) ) ;
#3262=ORIENTED_EDGE ( 'NONE', *, *, #4428, .F. ) ;
#3303=EDGE_CURVE ( 'NONE', #10528, #14639, #18751, .T. ) ;
#3315=ADVANCED_FACE ( 'NONE', ( #5120 ), #6783, .T. ) ;
#3325=CARTESIAN_POINT ( 'NONE',  ( 0.000000000000000000, 0.000000000000000000, 77.51594804401857175 ) ) ;
#3344=ORIENTED_EDGE ( 'NONE', *, *, #12459, .T. ) ;
#3353=CIRCLE ( 'NONE', #18101, 17.50000000000000711 ) ;
#3479=CARTESIAN_POINT ( 'NONE',  ( 0.000000000000000000, 19.79999999999999716, -78.50000000000000000 ) ) ;
#3485=EDGE_CURVE ( 'NONE', #5014, #19761, #15408, .T. ) ;
#3489=ORIENTED_EDGE ( 'NONE', *, *, #10673, .F. ) ;
#3517=CARTESIAN_POINT ( 'NONE',  ( 0.000000000000000000, 0.000000000000000000, -77.51594804401857175 ) ) ;
#3523=AXIS2_PLACEMENT_3D ( 'NONE', #14795, #4540, #21526 ) ;
#3536=DIRECTION ( 'NONE',  ( 0.000000000000000000, 0.000000000000000000, 1.000000000000000000 ) ) ;
#3546=CIRCLE ( 'NONE', #16861, 23.00000000000000000 ) ;
#3556=( LENGTH_UNIT ( ) NAMED_UNIT ( * ) SI_UNIT ( .MILLI., .METRE. ) );
#3588=CARTESIAN_POINT ( 'NONE',  ( 0.000000000000000000, 0.000000000000000000, 75.00000000000000000 ) ) ;
#3617=CARTESIAN_POINT ( 'NONE',  ( 0.000000000000000000, 0.000000000000000000, -77.51594804401857175 ) ) ;
#3642=FACE_OUTER_BOUND ( 'NONE', #11362, .T. ) ;
#3651=VERTEX_POINT ( 'NONE', #15280 ) ;
#3668=CIRCLE ( 'NONE', #19490, 20.99999999999999645 ) ;
#3695=CARTESIAN_POINT ( 'NONE',  ( -22.63401512838748175, 0.000000000000000000, -77.51594804401857175 ) ) ;
#3698=VECTOR ( 'NONE', #18705, 1000.000000000000000 ) ;
#3706=ORIENTED_EDGE ( 'NONE', *, *, #17805, .T. ) ;
#3719=EDGE_CURVE ( 'NONE', #16840, #4321, #11664, .T. ) ;
#3728=CARTESIAN_POINT ( 'NONE',  ( 0.000000000000000000, 22.63401512838748175, 77.51594804401857175 ) ) ;
#3772=ADVANCED_FACE ( 'NONE', ( #20650 ), #19189, .T. ) ;
#3800=DIRECTION ( 'NONE',  ( 0.000000000000000000, 1.000000000000000000, -0.000000000000000000 ) ) ;
#3801=ORIENTED_EDGE ( 'NONE', *, *, #7097, .T. ) ;
#3812=DIRECTION ( 'NONE',  ( 0.000000000000000000, 0.000000000000000000, -1.000000000000000000 ) ) ;
#3819=ORIENTED_EDGE ( 'NONE', *, *, #17680, .F. ) ;
#3829=DIRECTION ( 'NONE',  ( -1.000000000000000000, 0.000000000000000000, 0.000000000000000000 ) ) ;
#3851=FACE_OUTER_BOUND ( 'NONE', #11943, .T. ) ;
#3893=EDGE_CURVE ( 'NONE', #17518, #5014, #10425, .T. ) ;
#3898=LINE ( 'NONE', #17536, #9470 ) ;
#3905=ORIENTED_EDGE ( 'NONE', *, *, #7475, .T. ) ;
#3920=DIRECTION ( 'NONE',  ( 0.000000000000000000, 0.000000000000000000, -1.000000000000000000 ) ) ;
#3925=CARTESIAN_POINT ( 'NONE',  ( 0.000000000000000000, 0.000000000000000000, 75.00000000000000000 ) ) ;
#3978=FACE_OUTER_BOUND ( 'NONE', #4905, .T. ) ;
#3982=ORIENTED_EDGE ( 'NONE', *, *, #7373, .F. ) ;
#3988=ORIENTED_EDGE ( 'NONE', *, *, #13826, .F. ) ;
#3993=( NAMED_UNIT ( * ) SI_UNIT ( $, .STERADIAN. ) SOLID_ANGLE_UNIT ( ) );
#4005=AXIS2_PLACEMENT_3D ( 'NONE', #16157, #5901, #12988 ) ;
#4017=DIRECTION ( 'NONE',  ( 1.000000000000000000, 0.000000000000000000, 0.000000000000000000 ) ) ;
#4027=AXIS2_PLACEMENT_3D ( 'NONE', #12369, #14064, #14178 ) ;
#4029=DIRECTION ( 'NONE',  ( 1.000000000000000000, 6.982962677686266711E-15, 0.000000000000000000 ) ) ;
#4057=AXIS2_PLACEMENT_3D ( 'NONE', #21912, #8314, #3536 ) ;
#4065=CARTESIAN_POINT ( 'NONE',  ( 0.000000000000000000, 23.00000000000000355, -75.00000000000000000 ) ) ;
#4091=CARTESIAN_POINT ( 'NONE',  ( 0.000000000000000000, 0.000000000000000000, 69.99999999999998579 ) ) ;
#4114=DIRECTION ( 'NONE',  ( 0.000000000000000000, 0.000000000000000000, -1.000000000000000000 ) ) ;
#4143=CARTESIAN_POINT ( 'NONE',  ( 0.000000000000000000, 0.000000000000000000, 77.51594804401857175 ) ) ;
#4191=ORIENTED_EDGE ( 'NONE', *, *, #2321, .F. ) ;
#4223=EDGE_CURVE ( 'NONE', #13811, #1604, #10759, .T. ) ;
#4233=ORIENTED_EDGE ( 'NONE', *, *, #2395, .T. ) ;
#4238=DIRECTION ( 'NONE',  ( -1.000000000000000000, 0.000000000000000000, 0.000000000000000000 ) ) ;
#4239=ORIENTED_EDGE ( 'NONE', *, *, #22215, .F. ) ;
#4255=CARTESIAN_POINT ( 'NONE',  ( 0.000000000000000000, -23.00000000000000000, -55.00000000000000000 ) ) ;
#4280=DIRECTION ( 'NONE',  ( -0.000000000000000000, -0.000000000000000000, -1.000000000000000000 ) ) ;
#4289=FACE_OUTER_BOUND ( 'NONE', #18231, .T. ) ;
#4321=VERTEX_POINT ( 'NONE', #2521 ) ;
#4328=CARTESIAN_POINT ( 'NONE',  ( 0.000000000000000000, 0.000000000000000000, 77.51594804401857175 ) ) ;
#4346=CARTESIAN_POINT ( 'NONE',  ( 0.000000000000000000, 24.63401512838747820, 77.51594804401857175 ) ) ;
#4351=DIRECTION ( 'NONE',  ( -1.000000000000000000, 0.000000000000000000, 0.000000000000000000 ) ) ;
#4367=CIRCLE ( 'NONE', #16969, 3.000000000000002665 ) ;
#4379=DIRECTION ( 'NONE',  ( 1.083936797661035110E-15, 1.000000000000000000, 0.000000000000000000 ) ) ;
#4400=EDGE_CURVE ( 'NONE', #19675, #6063, #15779, .T. ) ;
#4401=CIRCLE ( 'NONE', #17353, 3.000000000000002665 ) ;
#4404=ORIENTED_EDGE ( 'NONE', *, *, #15523, .T. ) ;
#4417=AXIS2_PLACEMENT_3D ( 'NONE', #9597, #20139, #12966 ) ;
#4424=DIRECTION ( 'NONE',  ( 0.000000000000000000, 0.000000000000000000, 1.000000000000000000 ) ) ;
#4428=EDGE_CURVE ( 'NONE', #22217, #19675, #9512, .T. ) ;
#4454=ADVANCED_FACE ( 'NONE', ( #14366 ), #4972, .T. ) ;
#4460=AXIS2_PLACEMENT_3D ( 'NONE', #1551, #11797, #3224 ) ;
#4473=DIRECTION ( 'NONE',  ( 0.000000000000000000, 0.000000000000000000, -1.000000000000000000 ) ) ;
#4474=CIRCLE ( 'NONE', #522, 3.000000000000002665 ) ;
#4475=CARTESIAN_POINT ( 'NONE',  ( 0.000000000000000000, 21.00000000000000000, -75.00000000000000000 ) ) ;
#4479=MECHANICAL_DESIGN_GEOMETRIC_PRESENTATION_REPRESENTATION('',(#21017),#12765);
#4491=CARTESIAN_POINT ( 'NONE',  ( 0.000000000000000000, 0.000000000000000000, -55.00000000000000000 ) ) ;
#4531=DIRECTION ( 'NONE',  ( 0.000000000000000000, 0.000000000000000000, -1.000000000000000000 ) ) ;
#4540=DIRECTION ( 'NONE',  ( 0.000000000000000000, 0.000000000000000000, -1.000000000000000000 ) ) ;
#4549=ORIENTED_EDGE ( 'NONE', *, *, #6961, .T. ) ;
#4563=ADVANCED_FACE ( 'NONE', ( #622 ), #9295, .F. ) ;
#4585=DIRECTION ( 'NONE',  ( -1.000000000000000000, 0.000000000000000000, 0.000000000000000000 ) ) ;
#4602=VECTOR ( 'NONE', #9071, 1000.000000000000000 ) ;
#4624=CARTESIAN_POINT ( 'NONE',  ( 0.000000000000000000, 0.000000000000000000, 75.00000000000000000 ) ) ;
#4639=EDGE_CURVE ( 'NONE', #8365, #16840, #5448, .T. ) ;
#4648=DIRECTION ( 'NONE',  ( 0.000000000000000000, 0.000000000000000000, -1.000000000000000000 ) ) ;
#4649=DIRECTION ( 'NONE',  ( 0.000000000000000000, 0.000000000000000000, -1.000000000000000000 ) ) ;
#4681=DIRECTION ( 'NONE',  ( -2.162300680179923768E-16, -1.000000000000000000, 0.000000000000000000 ) ) ;
#4711=DIRECTION ( 'NONE',  ( 0.000000000000000000, 0.000000000000000000, -1.000000000000000000 ) ) ;
#4718=CARTESIAN_POINT ( 'NONE',  ( 0.000000000000000000, 0.000000000000000000, 77.51594804401857175 ) ) ;
#4738=ORIENTED_EDGE ( 'NONE', *, *, #19426, .T. ) ;
#4757=CIRCLE ( 'NONE', #1171, 23.00000000000000000 ) ;
#4758=CARTESIAN_POINT ( 'NONE',  ( 0.000000000000000000, 22.63401512838748175, -77.51594804401857175 ) ) ;
#4766=EDGE_CURVE ( 'NONE', #16533, #19761, #22097, .T. ) ;
#4778=AXIS2_PLACEMENT_3D ( 'NONE', #21318, #2203, #12679 ) ;
#4784=ORIENTED_EDGE ( 'NONE', *, *, #20402, .T. ) ;
#4805=CARTESIAN_POINT ( 'NONE',  ( -23.00000000000000000, 0.000000000000000000, -30.00000000000000000 ) ) ;
#4809=PLANE ( 'NONE',  #1899 ) ;
#4813=ORIENTED_EDGE ( 'NONE', *, *, #5651, .T. ) ;
#4850=AXIS2_PLACEMENT_3D ( 'NONE', #19232, #3812, #7433 ) ;
#4851=DIRECTION ( 'NONE',  ( 0.000000000000000000, 0.000000000000000000, -1.000000000000000000 ) ) ;
#4856=EDGE_CURVE ( 'NONE', #16533, #14290, #1856, .T. ) ;
#4858=EDGE_LOOP ( 'NONE', ( #20308, #6148, #21779, #21619, #19846, #15828 ) ) ;
#4898=AXIS2_PLACEMENT_3D ( 'NONE', #4718, #11489, #2918 ) ;
#4905=EDGE_LOOP ( 'NONE', ( #17625, #7710, #13023, #7597, #9429, #18268 ) ) ;
#4915=ADVANCED_FACE ( 'NONE', ( #17343 ), #13439, .F. ) ;
#4940=EDGE_CURVE ( 'NONE', #215, #21209, #15525, .T. ) ;
#4947=CARTESIAN_POINT ( 'NONE',  ( 0.000000000000000000, 17.50000000000000711, -60.00000000000000000 ) ) ;
#4961=LINE ( 'NONE', #1807, #3698 ) ;
#4970=ORIENTED_EDGE ( 'NONE', *, *, #17531, .T. ) ;
#4972=TOROIDAL_SURFACE ( 'NONE', #17574, 22.63401512838748175, 3.000000000000002665 ) ;
#4979=DIRECTION ( 'NONE',  ( 0.000000000000000000, 0.000000000000000000, 1.000000000000000000 ) ) ;
#5014=VERTEX_POINT ( 'NONE', #761 ) ;
#5027=LINE ( 'NONE', #13257, #16328 ) ;
#5065=ORIENTED_EDGE ( 'NONE', *, *, #15198, .F. ) ;
#5071=DIRECTION ( 'NONE',  ( -1.000000000000000000, 0.000000000000000000, 0.000000000000000000 ) ) ;
#5114=EDGE_LOOP ( 'NONE', ( #454, #22109, #292, #12348 ) ) ;
#5120=FACE_OUTER_BOUND ( 'NONE', #18374, .T. ) ;
#5121=ORIENTED_EDGE ( 'NONE', *, *, #10780, .F. ) ;
#5122=ADVANCED_FACE ( 'NONE', ( #14506 ), #21561, .F. ) ;
#5145=ORIENTED_EDGE ( 'NONE', *, *, #22146, .T. ) ;
#5182=AXIS2_PLACEMENT_3D ( 'NONE', #1960, #5556, #20632 ) ;
#5212=EDGE_LOOP ( 'NONE', ( #21846, #11544, #14180, #4549 ) ) ;
#5215=VECTOR ( 'NONE', #13771, 1000.000000000000000 ) ;
#5224=DIRECTION ( 'NONE',  ( 0.000000000000000000, 0.000000000000000000, -1.000000000000000000 ) ) ;
#5244=CARTESIAN_POINT ( 'NONE',  ( 0.000000000000000000, 0.000000000000000000, -30.00000000000000000 ) ) ;
#5263=ORIENTED_EDGE ( 'NONE', *, *, #6961, .F. ) ;
#5288=EDGE_CURVE ( 'NONE', #1564, #1604, #6892, .T. ) ;
#5320=EDGE_LOOP ( 'NONE', ( #21785, #9674, #18201, #2573 ) ) ;
#5326=EDGE_CURVE ( 'NONE', #2937, #11287, #4367, .T. ) ;
#5350=ORIENTED_EDGE ( 'NONE', *, *, #5326, .F. ) ;
#5354=CARTESIAN_POINT ( 'NONE',  ( 0.000000000000000000, 0.000000000000000000, 77.51594804401857175 ) ) ;
#5394=DIRECTION ( 'NONE',  ( -0.000000000000000000, -1.000000000000000000, -0.000000000000000000 ) ) ;
#5412=ADVANCED_FACE ( 'NONE', ( #6485 ), #13009, .T. ) ;
#5422=CARTESIAN_POINT ( 'NONE',  ( 0.000000000000000000, -23.00000000000000000, 75.00000000000000000 ) ) ;
#5430=ORIENTED_EDGE ( 'NONE', *, *, #17798, .T. ) ;
#5448=CIRCLE ( 'NONE', #4005, 17.50000000000000711 ) ;
#5468=LINE ( 'NONE', #20882, #20953 ) ;
#5472=LINE ( 'NONE', #2207, #7054 ) ;
#5473=AXIS2_PLACEMENT_3D ( 'NONE', #19796, #12846, #4379 ) ;
#5486=CARTESIAN_POINT ( 'NONE',  ( 0.000000000000000000, 23.00000000000000000, -30.00000000000000000 ) ) ;
#5487=ORIENTED_EDGE ( 'NONE', *, *, #17351, .F. ) ;
#5493=AXIS2_PLACEMENT_3D ( 'NONE', #10834, #595, #12421 ) ;
#5505=AXIS2_PLACEMENT_3D ( 'NONE', #1144, #20370, #15112 ) ;
#5512=ORIENTED_EDGE ( 'NONE', *, *, #5705, .F. ) ;
#5556=DIRECTION ( 'NONE',  ( -0.000000000000000000, -0.000000000000000000, -1.000000000000000000 ) ) ;
#5564=DIRECTION ( 'NONE',  ( 0.000000000000000000, 0.000000000000000000, -1.000000000000000000 ) ) ;
#5568=ORIENTED_EDGE ( 'NONE', *, *, #3719, .T. ) ;
#5573=DIRECTION ( 'NONE',  ( -1.000000000000000000, 0.000000000000000000, 0.000000000000000000 ) ) ;
#5582=PRESENTATION_STYLE_ASSIGNMENT (( #17412 ) ) ;
#5589=DIRECTION ( 'NONE',  ( 0.000000000000000000, 0.000000000000000000, 1.000000000000000000 ) ) ;
#5618=CARTESIAN_POINT ( 'NONE',  ( 0.000000000000000000, 0.000000000000000000, 69.99999999999998579 ) ) ;
#5633=CARTESIAN_POINT ( 'NONE',  ( 0.000000000000000000, 0.000000000000000000, -60.00000000000000000 ) ) ;
#5651=EDGE_CURVE ( 'NONE', #15752, #12803, #19815, .T. ) ;
#5653=CARTESIAN_POINT ( 'NONE',  ( 0.000000000000000000, 0.000000000000000000, -69.99999999999998579 ) ) ;
#5674=ORIENTED_EDGE ( 'NONE', *, *, #2395, .F. ) ;
#5686=APPLICATION_CONTEXT ( 'automotive_design' ) ;
#5691=DIRECTION ( 'NONE',  ( -1.083936797661035110E-15, -1.000000000000000000, 0.000000000000000000 ) ) ;
#5705=EDGE_CURVE ( 'NONE', #10234, #10093, #9075, .T. ) ;
#5721=FACE_OUTER_BOUND ( 'NONE', #1314, .T. ) ;
#5757=LINE ( 'NONE', #7576, #10191 ) ;
#5782=EDGE_CURVE ( 'NONE', #6063, #18247, #19467, .T. ) ;
#5787=CARTESIAN_POINT ( 'NONE',  ( 0.000000000000000000, 0.000000000000000000, -77.51594804401857175 ) ) ;
#5791=DIRECTION ( 'NONE',  ( 0.000000000000000000, 1.000000000000000000, 0.000000000000000000 ) ) ;
#5798=CARTESIAN_POINT ( 'NONE',  ( -21.63401512838747820, 0.000000000000000000, 77.51594804401857175 ) ) ;
#5815=CIRCLE ( 'NONE', #15527, 3.000000000000002665 ) ;
#5828=VECTOR ( 'NONE', #231, 1000.000000000000000 ) ;
#5839=EDGE_LOOP ( 'NONE', ( #2522, #2219, #4233, #22152 ) ) ;
#5879=VERTEX_POINT ( 'NONE', #14152 ) ;
#5889=CARTESIAN_POINT ( 'NONE',  ( 0.000000000000000000, -23.00000000000000000, -75.00000000000000000 ) ) ;
#5897=EDGE_CURVE ( 'NONE', #15809, #68, #82, .T. ) ;
#5901=DIRECTION ( 'NONE',  ( -0.000000000000000000, -0.000000000000000000, 1.000000000000000000 ) ) ;
#5911=ORIENTED_EDGE ( 'NONE', *, *, #9624, .F. ) ;
#5947=DIRECTION ( 'NONE',  ( -1.000000000000000000, 0.000000000000000000, 0.000000000000000000 ) ) ;
#5963=AXIS2_PLACEMENT_3D ( 'NONE', #21882, #19854, #7842 ) ;
#5976=LINE ( 'NONE', #11383, #9937 ) ;
#5993=ORIENTED_EDGE ( 'NONE', *, *, #16056, .T. ) ;
#6010=CARTESIAN_POINT ( 'NONE',  ( 0.000000000000000000, 0.000000000000000000, 60.00000000000001421 ) ) ;
#6034=ORIENTED_EDGE ( 'NONE', *, *, #17641, .F. ) ;
#6040=ORIENTED_EDGE ( 'NONE', *, *, #20887, .F. ) ;
#6052=DIRECTION ( 'NONE',  ( -1.000000000000000000, 0.000000000000000000, 0.000000000000000000 ) ) ;
#6063=VERTEX_POINT ( 'NONE', #17742 ) ;
#6072=CARTESIAN_POINT ( 'NONE',  ( -25.00000000000000000, 0.000000000000000000, -75.00000000000000000 ) ) ;
#6091=FACE_OUTER_BOUND ( 'NONE', #3051, .T. ) ;
#6121=CLOSED_SHELL ( 'NONE', ( #12847, #3315, #16155, #14625, #10429, #11066, #5412, #675, #13179, #7851, #4563, #9537, #4454, #11996, #15745, #20265, #9697, #5122, #8869, #6391, #11293, #2499, #19277, #18487, #15624, #16025, #1554, #19487, #1444, #20603, #18040, #4915, #9784, #11829, #20161, #12040, #9089, #18646, #787, #10106, #9424, #9813, #3772, #12158 ) ) ;
#6148=ORIENTED_EDGE ( 'NONE', *, *, #17705, .F. ) ;
#6153=DIRECTION ( 'NONE',  ( 0.000000000000000000, 0.000000000000000000, 1.000000000000000000 ) ) ;
#6162=AXIS2_PLACEMENT_3D ( 'NONE', #3069, #18507, #11196 ) ;
#6174=AXIS2_PLACEMENT_3D ( 'NONE', #8047, #2845, #21863 ) ;
#6192=TOROIDAL_SURFACE ( 'NONE', #10878, 22.63401512838748175, 3.000000000000002665 ) ;
#6208=AXIS2_PLACEMENT_3D ( 'NONE', #16866, #16639, #12105 ) ;
#6275=FACE_OUTER_BOUND ( 'NONE', #21422, .T. ) ;
#6279=AXIS2_PLACEMENT_3D ( 'NONE', #3029, #18689, #13394 ) ;
#6304=CARTESIAN_POINT ( 'NONE',  ( 0.000000000000000000, 0.000000000000000000, 77.51594804401857175 ) ) ;
#6318=FACE_OUTER_BOUND ( 'NONE', #16511, .T. ) ;
#6344=DIRECTION ( 'NONE',  ( 0.000000000000000000, 0.000000000000000000, 1.000000000000000000 ) ) ;
#6356=LINE ( 'NONE', #11534, #6984 ) ;
#6389=DIRECTION ( 'NONE',  ( 0.000000000000000000, 0.000000000000000000, -1.000000000000000000 ) ) ;
#6391=ADVANCED_FACE ( 'NONE', ( #19251 ), #12065, .F. ) ;
#6401=ORIENTED_EDGE ( 'NONE', *, *, #1237, .F. ) ;
#6407=VECTOR ( 'NONE', #9398, 1000.000000000000000 ) ;
#6429=DIRECTION ( 'NONE',  ( -1.000000000000000000, 0.000000000000000000, -0.000000000000000000 ) ) ;
#6443=DIRECTION ( 'NONE',  ( -0.000000000000000000, -0.000000000000000000, 1.000000000000000000 ) ) ;
#6467=CARTESIAN_POINT ( 'NONE',  ( 0.000000000000000000, 25.00000000000000000, 75.00000000000000000 ) ) ;
#6485=FACE_OUTER_BOUND ( 'NONE', #17914, .T. ) ;
#6541=CIRCLE ( 'NONE', #18035, 3.000000000000002665 ) ;
#6548=ORIENTED_EDGE ( 'NONE', *, *, #7297, .F. ) ;
#6569=VECTOR ( 'NONE', #14962, 1000.000000000000000 ) ;
#6588=VECTOR ( 'NONE', #5691, 1000.000000000000000 ) ;
#6607=AXIS2_PLACEMENT_3D ( 'NONE', #4143, #11022, #18106 ) ;
#6627=ORIENTED_EDGE ( 'NONE', *, *, #8856, .F. ) ;
#6677=AXIS2_PLACEMENT_3D ( 'NONE', #18028, #16226, #2707 ) ;
#6679=DIRECTION ( 'NONE',  ( 1.000000000000000000, 0.000000000000000000, 0.000000000000000000 ) ) ;
#6696=ORIENTED_EDGE ( 'NONE', *, *, #2239, .T. ) ;
#6701=LINE ( 'NONE', #1406, #15264 ) ;
#6718=ORIENTED_EDGE ( 'NONE', *, *, #20553, .F. ) ;
#6722=DIRECTION ( 'NONE',  ( -1.000000000000000000, 0.000000000000000000, 0.000000000000000000 ) ) ;
#6731=DIRECTION ( 'NONE',  ( 0.000000000000000000, 0.000000000000000000, -1.000000000000000000 ) ) ;
#6758=DIRECTION ( 'NONE',  ( -1.000000000000000000, 0.000000000000000000, -0.000000000000000000 ) ) ;
#6769=ORIENTED_EDGE ( 'NONE', *, *, #15276, .F. ) ;
#6783=TOROIDAL_SURFACE ( 'NONE', #8220, 22.63401512838748175, 3.000000000000002665 ) ;
#6791=CARTESIAN_POINT ( 'NONE',  ( 1.665334536937734811E-13, -23.00000000000000355, 75.00000000000000000 ) ) ;
#6802=EDGE_CURVE ( 'NONE', #7254, #19351, #5472, .T. ) ;
#6822=ORIENTED_EDGE ( 'NONE', *, *, #4639, .F. ) ;
#6827=CARTESIAN_POINT ( 'NONE',  ( 0.000000000000000000, 0.000000000000000000, 77.51594804401857175 ) ) ;
#6840=DIRECTION ( 'NONE',  ( -1.000000000000000000, -6.982962677686266711E-15, 0.000000000000000000 ) ) ;
#6841=FACE_OUTER_BOUND ( 'NONE', #1862, .T. ) ;
#6867=FACE_OUTER_BOUND ( 'NONE', #18912, .T. ) ;
#6892=CIRCLE ( 'NONE', #12288, 25.00000000000000000 ) ;
#6901=SURFACE_STYLE_FILL_AREA ( #1822 ) ;
#6917=CIRCLE ( 'NONE', #9791, 21.80000000000000071 ) ;
#6929=EDGE_CURVE ( 'NONE', #20645, #17987, #20687, .T. ) ;
#6950=CIRCLE ( 'NONE', #14509, 21.80000000000000071 ) ;
#6954=DIRECTION ( 'NONE',  ( -0.000000000000000000, -0.000000000000000000, -1.000000000000000000 ) ) ;
#6955=DIRECTION ( 'NONE',  ( -1.000000000000000000, 0.000000000000000000, 0.000000000000000000 ) ) ;
#6961=EDGE_CURVE ( 'NONE', #7178, #18886, #8501, .T. ) ;
#6972=AXIS2_PLACEMENT_3D ( 'NONE', #17217, #4711, #20573 ) ;
#6973=ORIENTED_EDGE ( 'NONE', *, *, #11247, .T. ) ;
#6984=VECTOR ( 'NONE', #15037, 1000.000000000000000 ) ;
#6985=FACE_OUTER_BOUND ( 'NONE', #16062, .T. ) ;
#7005=EDGE_LOOP ( 'NONE', ( #9926, #17501, #21095, #13788 ) ) ;
#7019=AXIS2_PLACEMENT_3D ( 'NONE', #2348, #14301, #8898 ) ;
#7035=ORIENTED_EDGE ( 'NONE', *, *, #21568, .T. ) ;
#7038=ORIENTED_EDGE ( 'NONE', *, *, #955, .F. ) ;
#7054=VECTOR ( 'NONE', #19206, 1000.000000000000000 ) ;
#7087=ORIENTED_EDGE ( 'NONE', *, *, #17083, .F. ) ;
#7097=EDGE_CURVE ( 'NONE', #20853, #2937, #2011, .T. ) ;
#7116=CARTESIAN_POINT ( 'NONE',  ( 0.000000000000000000, 0.000000000000000000, 75.00000000000000000 ) ) ;
#7127=CARTESIAN_POINT ( 'NONE',  ( 0.000000000000000000, 0.000000000000000000, -78.50000000000000000 ) ) ;
#7130=PRODUCT_DEFINITION ( 'UNKNOWN', '', #8511, #21564 ) ;
#7137=DIRECTION ( 'NONE',  ( 0.000000000000000000, 0.000000000000000000, -1.000000000000000000 ) ) ;
#7151=CARTESIAN_POINT ( 'NONE',  ( 0.000000000000000000, 25.00000000000000000, -75.00000000000000000 ) ) ;
#7178=VERTEX_POINT ( 'NONE', #20830 ) ;
#7199=ORIENTED_EDGE ( 'NONE', *, *, #11762, .T. ) ;
#7210=FACE_OUTER_BOUND ( 'NONE', #11890, .T. ) ;
#7226=DIRECTION ( 'NONE',  ( -1.000000000000000000, 0.000000000000000000, 0.000000000000000000 ) ) ;
#7247=DIRECTION ( 'NONE',  ( 0.000000000000000000, 0.000000000000000000, -1.000000000000000000 ) ) ;
#7254=VERTEX_POINT ( 'NONE', #14218 ) ;
#7256=ORIENTED_EDGE ( 'NONE', *, *, #13528, .F. ) ;
#7267=DIRECTION ( 'NONE',  ( -1.000000000000000000, 0.000000000000000000, -0.000000000000000000 ) ) ;
#7282=CARTESIAN_POINT ( 'NONE',  ( 0.000000000000000000, 0.000000000000000000, 78.50000000000000000 ) ) ;
#7286=( LENGTH_UNIT ( ) NAMED_UNIT ( * ) SI_UNIT ( .MILLI., .METRE. ) );
#7295=AXIS2_PLACEMENT_3D ( 'NONE', #5618, #12496, #15533 ) ;
#7297=EDGE_CURVE ( 'NONE', #862, #19977, #17477, .T. ) ;
#7303=VERTEX_POINT ( 'NONE', #371 ) ;
#7323=DIRECTION ( 'NONE',  ( -0.000000000000000000, -0.000000000000000000, -1.000000000000000000 ) ) ;
#7326=CIRCLE ( 'NONE', #4417, 23.00000000000000000 ) ;
#7342=VECTOR ( 'NONE', #4681, 1000.000000000000000 ) ;
#7361=AXIS2_PLACEMENT_3D ( 'NONE', #18768, #11903, #20323 ) ;
#7362=FACE_OUTER_BOUND ( 'NONE', #5839, .T. ) ;
#7373=EDGE_CURVE ( 'NONE', #14290, #19544, #16118, .T. ) ;
#7399=( NAMED_UNIT ( * ) SI_UNIT ( $, .STERADIAN. ) SOLID_ANGLE_UNIT ( ) );
#7426=UNCERTAINTY_MEASURE_WITH_UNIT (LENGTH_MEASURE( 1.000000000000000082E-05 ), #20271, 'distance_accuracy_value', 'NONE');
#7427=VECTOR ( 'NONE', #21267, 1000.000000000000000 ) ;
#7433=DIRECTION ( 'NONE',  ( -1.000000000000000000, 0.000000000000000000, 0.000000000000000000 ) ) ;
#7434=CYLINDRICAL_SURFACE ( 'NONE', #17339, 23.00000000000000000 ) ;
#7440=ORIENTED_EDGE ( 'NONE', *, *, #473, .F. ) ;
#7475=EDGE_CURVE ( 'NONE', #12803, #18886, #16451, .T. ) ;
#7503=VECTOR ( 'NONE', #21094, 1000.000000000000000 ) ;
#7508=ORIENTED_EDGE ( 'NONE', *, *, #20553, .T. ) ;
#7511=DIRECTION ( 'NONE',  ( -1.000000000000000000, 0.000000000000000000, 0.000000000000000000 ) ) ;
#7518=AXIS2_PLACEMENT_3D ( 'NONE', #2873, #1201, #4238 ) ;
#7519=CARTESIAN_POINT ( 'NONE',  ( 1.665334536937734811E-13, -24.63401512838747820, -77.51594804401857175 ) ) ;
#7528=DIRECTION ( 'NONE',  ( 0.000000000000000000, 0.000000000000000000, -1.000000000000000000 ) ) ;
#7561=ORIENTED_EDGE ( 'NONE', *, *, #10221, .F. ) ;
#7576=CARTESIAN_POINT ( 'NONE',  ( 0.000000000000000000, 21.00000000000000000, 75.00000000000000000 ) ) ;
#7584=EDGE_LOOP ( 'NONE', ( #10743, #12204, #17649, #3982 ) ) ;
#7596=VERTEX_POINT ( 'NONE', #17811 ) ;
#7597=ORIENTED_EDGE ( 'NONE', *, *, #21161, .F. ) ;
#7604=EDGE_CURVE ( 'NONE', #21555, #14126, #16336, .T. ) ;
#7621=AXIS2_PLACEMENT_3D ( 'NONE', #3325, #15284, #11668 ) ;
#7627=ORIENTED_EDGE ( 'NONE', *, *, #17083, .T. ) ;
#7643=EDGE_CURVE ( 'NONE', #2355, #18247, #5976, .T. ) ;
#7657=ORIENTED_EDGE ( 'NONE', *, *, #357, .T. ) ;
#7689=CIRCLE ( 'NONE', #20238, 21.63401512838748175 ) ;
#7710=ORIENTED_EDGE ( 'NONE', *, *, #11000, .F. ) ;
#7736=CARTESIAN_POINT ( 'NONE',  ( 0.000000000000000000, 17.50000000000000711, -24.99999999999999645 ) ) ;
#7739=ORIENTED_EDGE ( 'NONE', *, *, #20425, .F. ) ;
#7756=CARTESIAN_POINT ( 'NONE',  ( -22.63401512838748175, 0.000000000000000000, -77.51594804401857175 ) ) ;
#7760=VECTOR ( 'NONE', #16473, 1000.000000000000000 ) ;
#7769=ORIENTED_EDGE ( 'NONE', *, *, #3303, .T. ) ;
#7778=DIRECTION ( 'NONE',  ( 1.000000000000000000, 0.000000000000000000, -0.000000000000000000 ) ) ;
#7786=CARTESIAN_POINT ( 'NONE',  ( 0.000000000000000000, 0.000000000000000000, -75.00000000000000000 ) ) ;
#7808=ORIENTED_EDGE ( 'NONE', *, *, #20402, .F. ) ;
#7810=ORIENTED_EDGE ( 'NONE', *, *, #17232, .T. ) ;
#7842=DIRECTION ( 'NONE',  ( -1.000000000000000000, 0.000000000000000000, 0.000000000000000000 ) ) ;
#7845=ORIENTED_EDGE ( 'NONE', *, *, #14219, .F. ) ;
#7850=ORIENTED_EDGE ( 'NONE', *, *, #19047, .T. ) ;
#7851=ADVANCED_FACE ( 'NONE', ( #19915 ), #19275, .T. ) ;
#7872=DIRECTION ( 'NONE',  ( 0.000000000000000000, 0.000000000000000000, -1.000000000000000000 ) ) ;
#7967=DIRECTION ( 'NONE',  ( -1.000000000000000000, -0.000000000000000000, -0.000000000000000000 ) ) ;
#7978=DIRECTION ( 'NONE',  ( 1.000000000000000000, 4.408728476930466911E-15, -0.000000000000000000 ) ) ;
#7979=AXIS2_PLACEMENT_3D ( 'NONE', #19132, #8803, #7226 ) ;
#8020=DIRECTION ( 'NONE',  ( -1.000000000000000000, 0.000000000000000000, 0.000000000000000000 ) ) ;
#8047=CARTESIAN_POINT ( 'NONE',  ( 0.000000000000000000, 0.000000000000000000, 69.99999999999998579 ) ) ;
#8095=CARTESIAN_POINT ( 'NONE',  ( -17.50000000000000711, 0.000000000000000000, -55.00000000000000000 ) ) ;
#8113=MECHANICAL_DESIGN_GEOMETRIC_PRESENTATION_REPRESENTATION('',(#9910),#9545);
#8119=FACE_OUTER_BOUND ( 'NONE', #14390, .T. ) ;
#8133=DIRECTION ( 'NONE',  ( -0.000000000000000000, -0.000000000000000000, -1.000000000000000000 ) ) ;
#8163=EDGE_CURVE ( 'NONE', #7596, #16430, #11598, .T. ) ;
#8167=ORIENTED_EDGE ( 'NONE', *, *, #17263, .T. ) ;
#8187=ORIENTED_EDGE ( 'NONE', *, *, #4639, .T. ) ;
#8204=CARTESIAN_POINT ( 'NONE',  ( 0.000000000000000000, 0.000000000000000000, -78.50000000000000000 ) ) ;
#8211=ORIENTED_EDGE ( 'NONE', *, *, #11247, .F. ) ;
#8220=AXIS2_PLACEMENT_3D ( 'NONE', #6827, #13587, #1757 ) ;
#8313=CARTESIAN_POINT ( 'NONE',  ( -19.63401512838747820, 0.000000000000000000, -77.51594804401857175 ) ) ;
#8314=DIRECTION ( 'NONE',  ( -1.000000000000000000, -6.982962677686266711E-15, -0.000000000000000000 ) ) ;
#8318=ORIENTED_EDGE ( 'NONE', *, *, #3078, .F. ) ;
#8337=PLANE ( 'NONE',  #15914 ) ;
#8344=AXIS2_PLACEMENT_3D ( 'NONE', #1205, #9653, #1091 ) ;
#8365=VERTEX_POINT ( 'NONE', #7736 ) ;
#8382=TOROIDAL_SURFACE ( 'NONE', #12346, 24.63401512838747820, 3.000000000000000888 ) ;
#8383=DIRECTION ( 'NONE',  ( 0.000000000000000000, 0.000000000000000000, 1.000000000000000000 ) ) ;
#8418=CARTESIAN_POINT ( 'NONE',  ( 0.000000000000000000, 0.000000000000000000, 75.00000000000000000 ) ) ;
#8425=DIRECTION ( 'NONE',  ( -1.000000000000000000, 0.000000000000000000, 0.000000000000000000 ) ) ;
#8439=AXIS2_PLACEMENT_3D ( 'NONE', #5354, #5589, #20772 ) ;
#8443=ORIENTED_EDGE ( 'NONE', *, *, #19047, .F. ) ;
#8455=( GEOMETRIC_REPRESENTATION_CONTEXT ( 3 ) GLOBAL_UNCERTAINTY_ASSIGNED_CONTEXT ( ( #2227 ) ) GLOBAL_UNIT_ASSIGNED_CONTEXT ( ( #7286, #8751, #7399 ) ) REPRESENTATION_CONTEXT ( 'NONE', 'WORKASPACE' ) );
#8475=CIRCLE ( 'NONE', #16018, 21.00000000000000000 ) ;
#8476=DIRECTION ( 'NONE',  ( -2.162300680179923768E-16, -1.000000000000000000, 0.000000000000000000 ) ) ;
#8501=CIRCLE ( 'NONE', #5963, 23.00000000000000000 ) ;
#8511=PRODUCT_DEFINITION_FORMATION_WITH_SPECIFIED_SOURCE ( 'ANY', '', #17154, .NOT_KNOWN. ) ;
#8537=CARTESIAN_POINT ( 'NONE',  ( 0.000000000000000000, 0.000000000000000000, -24.99999999999999645 ) ) ;
#8555=ORIENTED_EDGE ( 'NONE', *, *, #15991, .F. ) ;
#8566=LINE ( 'NONE', #3479, #12062 ) ;
#8582=AXIS2_PLACEMENT_3D ( 'NONE', #21784, #18861, #10317 ) ;
#8583=CARTESIAN_POINT ( 'NONE',  ( 0.000000000000000000, 23.00000000000000000, -69.99999999999998579 ) ) ;
#8626=ORIENTED_EDGE ( 'NONE', *, *, #7604, .T. ) ;
#8670=CARTESIAN_POINT ( 'NONE',  ( 1.526556658859590243E-13, -21.80000000000000071, -78.50000000000000000 ) ) ;
#8701=CIRCLE ( 'NONE', #18401, 3.000000000000002665 ) ;
#8719=VERTEX_POINT ( 'NONE', #642 ) ;
#8729=DIRECTION ( 'NONE',  ( 0.000000000000000000, -0.000000000000000000, 1.000000000000000000 ) ) ;
#8739=EDGE_CURVE ( 'NONE', #1956, #1152, #2247, .T. ) ;
#8741=CARTESIAN_POINT ( 'NONE',  ( 0.000000000000000000, -17.50000000000000711, -24.99999999999999645 ) ) ;
#8746=DIRECTION ( 'NONE',  ( 0.000000000000000000, 0.000000000000000000, -1.000000000000000000 ) ) ;
#8751=( NAMED_UNIT ( * ) PLANE_ANGLE_UNIT ( ) SI_UNIT ( $, .RADIAN. ) );
#8753=CIRCLE ( 'NONE', #2973, 3.000000000000002665 ) ;
#8757=DIRECTION ( 'NONE',  ( -1.000000000000000000, 0.000000000000000000, 0.000000000000000000 ) ) ;
#8772=ORIENTED_EDGE ( 'NONE', *, *, #5288, .T. ) ;
#8777=AXIS2_PLACEMENT_3D ( 'NONE', #2533, #19203, #7511 ) ;
#8785=CARTESIAN_POINT ( 'NONE',  ( 0.000000000000000000, 0.000000000000000000, -30.00000000000000000 ) ) ;
#8803=DIRECTION ( 'NONE',  ( 0.000000000000000000, 0.000000000000000000, -1.000000000000000000 ) ) ;
#8804=DIRECTION ( 'NONE',  ( 1.000000000000000000, 0.000000000000000000, -0.000000000000000000 ) ) ;
#8816=DIRECTION ( 'NONE',  ( 0.000000000000000000, 0.000000000000000000, 1.000000000000000000 ) ) ;
#8835=ORIENTED_EDGE ( 'NONE', *, *, #5705, .T. ) ;
#8856=EDGE_CURVE ( 'NONE', #14290, #5879, #19973, .T. ) ;
#8857=AXIS2_PLACEMENT_3D ( 'NONE', #3728, #21163, #19476 ) ;
#8869=ADVANCED_FACE ( 'NONE', ( #13128 ), #11327, .F. ) ;
#8881=EDGE_LOOP ( 'NONE', ( #1535, #12055, #2110, #9182 ) ) ;
#8887=CARTESIAN_POINT ( 'NONE',  ( 1.526556658859590243E-13, -20.99999999999999645, -69.99999999999998579 ) ) ;
#8898=DIRECTION ( 'NONE',  ( -1.000000000000000000, 0.000000000000000000, 0.000000000000000000 ) ) ;
#8905=ORIENTED_EDGE ( 'NONE', *, *, #1573, .F. ) ;
#8926=CARTESIAN_POINT ( 'NONE',  ( 0.000000000000000000, 0.000000000000000000, 77.51594804401857175 ) ) ;
#8934=DIRECTION ( 'NONE',  ( -1.000000000000000000, 0.000000000000000000, 0.000000000000000000 ) ) ;
#8955=DIRECTION ( 'NONE',  ( -0.000000000000000000, -0.000000000000000000, -1.000000000000000000 ) ) ;
#8970=FILL_AREA_STYLE_COLOUR ( '', #16000 ) ;
#8995=ORIENTED_EDGE ( 'NONE', *, *, #20384, .F. ) ;
#9005=PLANE ( 'NONE',  #19575 ) ;
#9062=DIRECTION ( 'NONE',  ( -1.000000000000000000, 0.000000000000000000, 0.000000000000000000 ) ) ;
#9071=DIRECTION ( 'NONE',  ( -2.162300680179923768E-16, -1.000000000000000000, 0.000000000000000000 ) ) ;
#9075=LINE ( 'NONE', #10430, #20545 ) ;
#9076=CIRCLE ( 'NONE', #19480, 3.000000000000002665 ) ;
#9089=ADVANCED_FACE ( 'NONE', ( #1829 ), #6192, .T. ) ;
#9100=ORIENTED_EDGE ( 'NONE', *, *, #357, .F. ) ;
#9121=AXIS2_PLACEMENT_3D ( 'NONE', #20436, #6840, #6731 ) ;
#9158=CARTESIAN_POINT ( 'NONE',  ( 0.000000000000000000, 0.000000000000000000, -77.51594804401857175 ) ) ;
#9182=ORIENTED_EDGE ( 'NONE', *, *, #21371, .F. ) ;
#9218=DIRECTION ( 'NONE',  ( 0.000000000000000000, 0.000000000000000000, 1.000000000000000000 ) ) ;
#9228=EDGE_CURVE ( 'NONE', #18886, #10528, #4757, .T. ) ;
#9234=CARTESIAN_POINT ( 'NONE',  ( 0.000000000000000000, 23.00000000000000000, -24.99999999999999289 ) ) ;
#9254=ORIENTED_EDGE ( 'NONE', *, *, #4400, .T. ) ;
#9259=CARTESIAN_POINT ( 'NONE',  ( 0.000000000000000000, -23.00000000000000000, 75.00000000000000000 ) ) ;
#9295=CYLINDRICAL_SURFACE ( 'NONE', #18764, 20.99999999999999645 ) ;
#9296=CARTESIAN_POINT ( 'NONE',  ( -20.99999999999999645, 0.000000000000000000, 69.99999999999998579 ) ) ;
#9353=DIRECTION ( 'NONE',  ( 4.845403715540889009E-30, -6.938893903907222461E-16, -1.000000000000000000 ) ) ;
#9359=DIRECTION ( 'NONE',  ( -1.000000000000000000, 0.000000000000000000, 0.000000000000000000 ) ) ;
#9388=LINE ( 'NONE', #5889, #814 ) ;
#9398=DIRECTION ( 'NONE',  ( -0.000000000000000000, -0.000000000000000000, -1.000000000000000000 ) ) ;
#9424=ADVANCED_FACE ( 'NONE', ( #3851 ), #14558, .F. ) ;
#9429=ORIENTED_EDGE ( 'NONE', *, *, #21404, .F. ) ;
#9431=EDGE_CURVE ( 'NONE', #15752, #7178, #2056, .T. ) ;
#9444=DIRECTION ( 'NONE',  ( -1.000000000000000000, 0.000000000000000000, 0.000000000000000000 ) ) ;
#9459=VECTOR ( 'NONE', #17931, 1000.000000000000000 ) ;
#9469=TOROIDAL_SURFACE ( 'NONE', #13778, 22.63401512838748175, 3.000000000000002665 ) ;
#9470=VECTOR ( 'NONE', #10774, 1000.000000000000000 ) ;
#9512=LINE ( 'NONE', #14470, #6407 ) ;
#9513=DIRECTION ( 'NONE',  ( 0.000000000000000000, 0.000000000000000000, -1.000000000000000000 ) ) ;
#9520=CIRCLE ( 'NONE', #22091, 19.63401512838747820 ) ;
#9537=ADVANCED_FACE ( 'NONE', ( #7362 ), #8382, .F. ) ;
#9538=ORIENTED_EDGE ( 'NONE', *, *, #14886, .T. ) ;
#9545=( GEOMETRIC_REPRESENTATION_CONTEXT ( 3 ) GLOBAL_UNCERTAINTY_ASSIGNED_CONTEXT ( ( #7426 ) ) GLOBAL_UNIT_ASSIGNED_CONTEXT ( ( #20271, #20610, #11746 ) ) REPRESENTATION_CONTEXT ( 'NONE', 'WORKASPACE' ) );
#9550=DIRECTION ( 'NONE',  ( -0.000000000000000000, -0.000000000000000000, -1.000000000000000000 ) ) ;
#9556=DIRECTION ( 'NONE',  ( -1.000000000000000000, 0.000000000000000000, 0.000000000000000000 ) ) ;
#9588=VECTOR ( 'NONE', #18026, 1000.000000000000000 ) ;
#9597=CARTESIAN_POINT ( 'NONE',  ( 0.000000000000000000, 0.000000000000000000, -30.00000000000000000 ) ) ;
#9611=LINE ( 'NONE', #16580, #7760 ) ;
#9624=EDGE_CURVE ( 'NONE', #5879, #13000, #5757, .T. ) ;
#9643=ORIENTED_EDGE ( 'NONE', *, *, #1237, .T. ) ;
#9647=EDGE_LOOP ( 'NONE', ( #3489, #15345, #19634, #19349, #8835, #20221 ) ) ;
#9653=DIRECTION ( 'NONE',  ( -0.000000000000000000, -0.000000000000000000, -1.000000000000000000 ) ) ;
#9674=ORIENTED_EDGE ( 'NONE', *, *, #6929, .T. ) ;
#9688=DIRECTION ( 'NONE',  ( 0.000000000000000000, 0.000000000000000000, -1.000000000000000000 ) ) ;
#9697=ADVANCED_FACE ( 'NONE', ( #6091 ), #2715, .T. ) ;
#9702=EDGE_CURVE ( 'NONE', #12646, #2355, #7326, .T. ) ;
#9704=CARTESIAN_POINT ( 'NONE',  ( 0.000000000000000000, 0.000000000000000000, 77.51594804401857175 ) ) ;
#9719=DIRECTION ( 'NONE',  ( -0.000000000000000000, -1.000000000000000000, -0.000000000000000000 ) ) ;
#9727=CARTESIAN_POINT ( 'NONE',  ( -24.63401512838747820, 0.000000000000000000, -77.51594804401857175 ) ) ;
#9756=EDGE_LOOP ( 'NONE', ( #18070, #10634, #18294, #164 ) ) ;
#9761=DIRECTION ( 'NONE',  ( -1.000000000000000000, 0.000000000000000000, 0.000000000000000000 ) ) ;
#9769=CARTESIAN_POINT ( 'NONE',  ( 0.000000000000000000, 17.50000000000000711, -30.00000000000000000 ) ) ;
#9772=DIRECTION ( 'NONE',  ( -1.000000000000000000, 0.000000000000000000, 0.000000000000000000 ) ) ;
#9773=AXIS2_PLACEMENT_3D ( 'NONE', #5633, #20280, #21974 ) ;
#9774=CARTESIAN_POINT ( 'NONE',  ( 0.000000000000000000, 19.79999999999999716, -78.50000000000000000 ) ) ;
#9784=ADVANCED_FACE ( 'NONE', ( #4289 ), #16460, .F. ) ;
#9791=AXIS2_PLACEMENT_3D ( 'NONE', #17768, #7528, #2221 ) ;
#9800=AXIS2_PLACEMENT_3D ( 'NONE', #17851, #19190, #12558 ) ;
#9804=CARTESIAN_POINT ( 'NONE',  ( 1.526556658859590243E-13, -21.00000000000000000, 75.00000000000000000 ) ) ;
#9813=ADVANCED_FACE ( 'NONE', ( #6318 ), #17368, .T. ) ;
#9862=DIRECTION ( 'NONE',  ( -1.000000000000000000, 0.000000000000000000, 0.000000000000000000 ) ) ;
#9888=CARTESIAN_POINT ( 'NONE',  ( -20.99999999999999645, 0.000000000000000000, -69.99999999999998579 ) ) ;
#9910=STYLED_ITEM ( 'NONE', ( #21965 ), #21655 ) ;
#9926=ORIENTED_EDGE ( 'NONE', *, *, #17888, .F. ) ;
#9928=AXIS2_PLACEMENT_3D ( 'NONE', #7116, #13982, #12282 ) ;
#9931=DIRECTION ( 'NONE',  ( 0.000000000000000000, 0.000000000000000000, -1.000000000000000000 ) ) ;
#9937=VECTOR ( 'NONE', #21717, 1000.000000000000000 ) ;
#9949=DIRECTION ( 'NONE',  ( -1.000000000000000000, 0.000000000000000000, 0.000000000000000000 ) ) ;
#9957=DIRECTION ( 'NONE',  ( 1.000000000000000000, 0.000000000000000000, 0.000000000000000000 ) ) ;
#9991=CYLINDRICAL_SURFACE ( 'NONE', #17389, 23.00000000000000000 ) ;
#10013=VERTEX_POINT ( 'NONE', #2928 ) ;
#10073=ORIENTED_EDGE ( 'NONE', *, *, #2267, .T. ) ;
#10093=VERTEX_POINT ( 'NONE', #20037 ) ;
#10106=ADVANCED_FACE ( 'NONE', ( #18260 ), #2824, .T. ) ;
#10131=AXIS2_PLACEMENT_3D ( 'NONE', #4491, #17797, #19573 ) ;
#10148=ORIENTED_EDGE ( 'NONE', *, *, #7643, .F. ) ;
#10191=VECTOR ( 'NONE', #14442, 1000.000000000000000 ) ;
#10211=TOROIDAL_SURFACE ( 'NONE', #2640, 24.63401512838747820, 3.000000000000000888 ) ;
#10221=EDGE_CURVE ( 'NONE', #8365, #12271, #4961, .T. ) ;
#10231=EDGE_LOOP ( 'NONE', ( #19433, #12314, #11695, #9254 ) ) ;
#10234=VERTEX_POINT ( 'NONE', #17345 ) ;
#10244=CIRCLE ( 'NONE', #5182, 25.00000000000000000 ) ;
#10273=ORIENTED_EDGE ( 'NONE', *, *, #21568, .F. ) ;
#10282=CARTESIAN_POINT ( 'NONE',  ( 0.000000000000000000, 23.00000000000000000, 75.00000000000000000 ) ) ;
#10292=VECTOR ( 'NONE', #4280, 1000.000000000000000 ) ;
#10317=DIRECTION ( 'NONE',  ( -1.000000000000000000, 0.000000000000000000, 0.000000000000000000 ) ) ;
#10318=ORIENTED_EDGE ( 'NONE', *, *, #18214, .F. ) ;
#10331=DIRECTION ( 'NONE',  ( -0.000000000000000000, -0.000000000000000000, -1.000000000000000000 ) ) ;
#10339=ORIENTED_EDGE ( 'NONE', *, *, #17263, .F. ) ;
#10343=ORIENTED_EDGE ( 'NONE', *, *, #21404, .T. ) ;
#10351=EDGE_CURVE ( 'NONE', #20901, #15752, #22187, .T. ) ;
#10357=DIRECTION ( 'NONE',  ( 0.000000000000000000, 1.000000000000000000, 0.000000000000000000 ) ) ;
#10358=CARTESIAN_POINT ( 'NONE',  ( 0.000000000000000000, 0.000000000000000000, 75.00000000000000000 ) ) ;
#10373=FACE_OUTER_BOUND ( 'NONE', #12248, .T. ) ;
#10425=LINE ( 'NONE', #8741, #4602 ) ;
#10429=ADVANCED_FACE ( 'NONE', ( #10373 ), #9469, .T. ) ;
#10430=CARTESIAN_POINT ( 'NONE',  ( 0.000000000000000000, 19.79999999999999716, 78.50000000000000000 ) ) ;
#10434=SHAPE_REPRESENTATION_RELATIONSHIP ( 'NONE' , 'NONE' ,  #13052, #11503 ) ;
#10465=DIRECTION ( 'NONE',  ( 0.000000000000000000, 0.000000000000000000, -1.000000000000000000 ) ) ;
#10498=VECTOR ( 'NONE', #13980, 1000.000000000000000 ) ;
#10528=VERTEX_POINT ( 'NONE', #8583 ) ;
#10535=ORIENTED_EDGE ( 'NONE', *, *, #19326, .T. ) ;
#10560=VERTEX_POINT ( 'NONE', #17236 ) ;
#10579=CIRCLE ( 'NONE', #4460, 17.50000000000000711 ) ;
#10580=DIRECTION ( 'NONE',  ( 0.000000000000000000, 0.000000000000000000, -1.000000000000000000 ) ) ;
#10616=CIRCLE ( 'NONE', #4850, 19.63401512838747820 ) ;
#10634=ORIENTED_EDGE ( 'NONE', *, *, #20690, .F. ) ;
#10673=EDGE_CURVE ( 'NONE', #13837, #21809, #6950, .T. ) ;
#10695=DIRECTION ( 'NONE',  ( -1.000000000000000000, 0.000000000000000000, 0.000000000000000000 ) ) ;
#10743=ORIENTED_EDGE ( 'NONE', *, *, #4856, .F. ) ;
#10749=CARTESIAN_POINT ( 'NONE',  ( 0.000000000000000000, 21.63401512838747820, 77.51594804401857175 ) ) ;
#10759=LINE ( 'NONE', #17624, #7503 ) ;
#10770=DIRECTION ( 'NONE',  ( -0.000000000000000000, -1.000000000000000000, -0.000000000000000000 ) ) ;
#10774=DIRECTION ( 'NONE',  ( 6.982962677686266711E-15, -1.000000000000000000, 0.000000000000000000 ) ) ;
#10780=EDGE_CURVE ( 'NONE', #20645, #21551, #8753, .T. ) ;
#10787=CARTESIAN_POINT ( 'NONE',  ( 0.000000000000000000, 0.000000000000000000, -75.00000000000000000 ) ) ;
#10788=ORIENTED_EDGE ( 'NONE', *, *, #17641, .T. ) ;
#10808=ORIENTED_EDGE ( 'NONE', *, *, #17805, .F. ) ;
#10834=CARTESIAN_POINT ( 'NONE',  ( 0.000000000000000000, 0.000000000000000000, 60.00000000000001421 ) ) ;
#10838=AXIS2_PLACEMENT_3D ( 'NONE', #11635, #4648, #15133 ) ;
#10875=CARTESIAN_POINT ( 'NONE',  ( 0.000000000000000000, 23.00000000000000000, -60.00000000000000000 ) ) ;
#10878=AXIS2_PLACEMENT_3D ( 'NONE', #3517, #7137, #22209 ) ;
#10894=EDGE_LOOP ( 'NONE', ( #4738, #22182, #16166, #22005 ) ) ;
#10908=DIRECTION ( 'NONE',  ( -0.000000000000000000, -0.000000000000000000, -1.000000000000000000 ) ) ;
#10912=AXIS2_PLACEMENT_3D ( 'NONE', #14516, #21238, #6052 ) ;
#10913=CIRCLE ( 'NONE', #13798, 17.50000000000000711 ) ;
#10958=ORIENTED_EDGE ( 'NONE', *, *, #3078, .T. ) ;
#10968=CARTESIAN_POINT ( 'NONE',  ( 0.000000000000000000, 0.000000000000000000, 75.00000000000000000 ) ) ;
#10990=ORIENTED_EDGE ( 'NONE', *, *, #2596, .T. ) ;
#11000=EDGE_CURVE ( 'NONE', #3205, #19675, #20094, .T. ) ;
#11006=AXIS2_PLACEMENT_3D ( 'NONE', #4328, #2974, #18411 ) ;
#11022=DIRECTION ( 'NONE',  ( 0.000000000000000000, 0.000000000000000000, 1.000000000000000000 ) ) ;
#11053=CARTESIAN_POINT ( 'NONE',  ( -23.00000000000000000, 0.000000000000000000, 75.00000000000000000 ) ) ;
#11066=ADVANCED_FACE ( 'NONE', ( #11895 ), #10211, .F. ) ;
#11140=ORIENTED_EDGE ( 'NONE', *, *, #3893, .F. ) ;
#11160=CARTESIAN_POINT ( 'NONE',  ( 0.000000000000000000, 23.00000000000000000, 75.00000000000000000 ) ) ;
#11196=DIRECTION ( 'NONE',  ( -1.000000000000000000, 0.000000000000000000, 0.000000000000000000 ) ) ;
#11236=DIRECTION ( 'NONE',  ( 0.000000000000000000, 0.000000000000000000, -1.000000000000000000 ) ) ;
#11247=EDGE_CURVE ( 'NONE', #862, #10234, #1208, .T. ) ;
#11256=CARTESIAN_POINT ( 'NONE',  ( 1.526556658859590243E-13, -21.00000000000000000, -75.00000000000000000 ) ) ;
#11265=DIRECTION ( 'NONE',  ( -0.000000000000000000, -0.000000000000000000, -1.000000000000000000 ) ) ;
#11287=VERTEX_POINT ( 'NONE', #21676 ) ;
#11293=ADVANCED_FACE ( 'NONE', ( #22010 ), #9991, .F. ) ;
#11306=CARTESIAN_POINT ( 'NONE',  ( -20.99999999999999645, 0.000000000000000000, -60.00000000000001421 ) ) ;
#11327=CYLINDRICAL_SURFACE ( 'NONE', #19488, 23.00000000000000000 ) ;
#11334=ORIENTED_EDGE ( 'NONE', *, *, #16505, .T. ) ;
#11338=ORIENTED_EDGE ( 'NONE', *, *, #18602, .F. ) ;
#11355=CARTESIAN_POINT ( 'NONE',  ( -23.00000000000000000, 0.000000000000000000, -24.99999999999999645 ) ) ;
#11362=EDGE_LOOP ( 'NONE', ( #12567, #19213, #2686, #11764, #5263, #19302 ) ) ;
#11371=AXIS2_PLACEMENT_3D ( 'NONE', #8926, #8816, #15792 ) ;
#11383=CARTESIAN_POINT ( 'NONE',  ( 0.000000000000000000, 23.00000000000000000, 75.00000000000000000 ) ) ;
#11407=LINE ( 'NONE', #18276, #920 ) ;
#11436=CARTESIAN_POINT ( 'NONE',  ( 0.000000000000000000, 0.000000000000000000, 75.00000000000000000 ) ) ;
#11475=EDGE_CURVE ( 'NONE', #16180, #16938, #21691, .T. ) ;
#11489=DIRECTION ( 'NONE',  ( 0.000000000000000000, 0.000000000000000000, 1.000000000000000000 ) ) ;
#11503=ADVANCED_BREP_SHAPE_REPRESENTATION ( '', ( #21655, #6677 ), #8455 ) ;
#11534=CARTESIAN_POINT ( 'NONE',  ( 0.000000000000000000, -23.00000000000000000, 75.00000000000000000 ) ) ;
#11544=ORIENTED_EDGE ( 'NONE', *, *, #5651, .F. ) ;
#11598=LINE ( 'NONE', #9804, #13897 ) ;
#11606=ORIENTED_EDGE ( 'NONE', *, *, #7297, .T. ) ;
#11635=CARTESIAN_POINT ( 'NONE',  ( 0.000000000000000000, 0.000000000000000000, -24.99999999999999645 ) ) ;
#11664=LINE ( 'NONE', #1421, #15051 ) ;
#11668=DIRECTION ( 'NONE',  ( -1.000000000000000000, 0.000000000000000000, 0.000000000000000000 ) ) ;
#11685=CARTESIAN_POINT ( 'NONE',  ( -17.50000000000000711, 0.000000000000000000, -55.00000000000000000 ) ) ;
#11695=ORIENTED_EDGE ( 'NONE', *, *, #4428, .T. ) ;
#11735=ORIENTED_EDGE ( 'NONE', *, *, #10351, .T. ) ;
#11746=( NAMED_UNIT ( * ) SI_UNIT ( $, .STERADIAN. ) SOLID_ANGLE_UNIT ( ) );
#11754=DIRECTION ( 'NONE',  ( 0.000000000000000000, 0.000000000000000000, 1.000000000000000000 ) ) ;
#11762=EDGE_CURVE ( 'NONE', #19351, #1956, #12715, .T. ) ;
#11764=ORIENTED_EDGE ( 'NONE', *, *, #9228, .F. ) ;
#11795=DIRECTION ( 'NONE',  ( -0.000000000000000000, -0.000000000000000000, 1.000000000000000000 ) ) ;
#11797=DIRECTION ( 'NONE',  ( -0.000000000000000000, -0.000000000000000000, 1.000000000000000000 ) ) ;
#11829=ADVANCED_FACE ( 'NONE', ( #12151 ), #2233, .T. ) ;
#11833=ORIENTED_EDGE ( 'NONE', *, *, #1573, .T. ) ;
#11854=SURFACE_SIDE_STYLE ('',( #6901 ) ) ;
#11890=EDGE_LOOP ( 'NONE', ( #8187, #5568, #14308, #7561 ) ) ;
#11895=FACE_OUTER_BOUND ( 'NONE', #1343, .T. ) ;
#11901=DIRECTION ( 'NONE',  ( -0.000000000000000000, -1.000000000000000000, -0.000000000000000000 ) ) ;
#11903=DIRECTION ( 'NONE',  ( 0.000000000000000000, 0.000000000000000000, 1.000000000000000000 ) ) ;
#11919=ORIENTED_EDGE ( 'NONE', *, *, #13698, .F. ) ;
#11943=EDGE_LOOP ( 'NONE', ( #7256, #14821, #2185, #6040 ) ) ;
#11956=AXIS2_PLACEMENT_3D ( 'NONE', #12155, #19012, #19776 ) ;
#11972=AXIS2_PLACEMENT_3D ( 'NONE', #9704, #13298, #18481 ) ;
#11996=ADVANCED_FACE ( 'NONE', ( #444 ), #14298, .F. ) ;
#12006=CARTESIAN_POINT ( 'NONE',  ( 0.000000000000000000, 0.000000000000000000, -60.00000000000000000 ) ) ;
#12040=ADVANCED_FACE ( 'NONE', ( #6275 ), #12926, .F. ) ;
#12055=ORIENTED_EDGE ( 'NONE', *, *, #20398, .T. ) ;
#12062=VECTOR ( 'NONE', #10357, 1000.000000000000000 ) ;
#12065=CYLINDRICAL_SURFACE ( 'NONE', #9928, 23.00000000000000000 ) ;
#12094=ORIENTED_EDGE ( 'NONE', *, *, #550, .T. ) ;
#12097=ORIENTED_EDGE ( 'NONE', *, *, #17705, .T. ) ;
#12105=DIRECTION ( 'NONE',  ( 0.000000000000000000, 0.000000000000000000, 1.000000000000000000 ) ) ;
#12126=DIRECTION ( 'NONE',  ( -1.000000000000000000, 0.000000000000000000, 0.000000000000000000 ) ) ;
#12149=EDGE_CURVE ( 'NONE', #16621, #16938, #16312, .T. ) ;
#12151=FACE_OUTER_BOUND ( 'NONE', #20261, .T. ) ;
#12155=CARTESIAN_POINT ( 'NONE',  ( 0.000000000000000000, 0.000000000000000000, -75.00000000000000000 ) ) ;
#12158=ADVANCED_FACE ( 'NONE', ( #21348 ), #14179, .F. ) ;
#12162=ORIENTED_EDGE ( 'NONE', *, *, #17409, .T. ) ;
#12169=VECTOR ( 'NONE', #20424, 1000.000000000000000 ) ;
#12179=CIRCLE ( 'NONE', #7518, 19.63401512838747820 ) ;
#12204=ORIENTED_EDGE ( 'NONE', *, *, #4766, .T. ) ;
#12208=CARTESIAN_POINT ( 'NONE',  ( 0.000000000000000000, 23.00000000000000000, 69.99999999999998579 ) ) ;
#12248=EDGE_LOOP ( 'NONE', ( #7627, #2722, #21380, #17017 ) ) ;
#12271=VERTEX_POINT ( 'NONE', #9769 ) ;
#12275=EDGE_CURVE ( 'NONE', #21809, #10093, #22052, .T. ) ;
#12282=DIRECTION ( 'NONE',  ( -1.000000000000000000, 0.000000000000000000, 0.000000000000000000 ) ) ;
#12283=AXIS2_PLACEMENT_3D ( 'NONE', #15885, #17344, #11754 ) ;
#12288=AXIS2_PLACEMENT_3D ( 'NONE', #3106, #18756, #6722 ) ;
#12314=ORIENTED_EDGE ( 'NONE', *, *, #13126, .F. ) ;
#12325=PLANE ( 'NONE',  #21660 ) ;
#12346=AXIS2_PLACEMENT_3D ( 'NONE', #9158, #7247, #16127 ) ;
#12348=ORIENTED_EDGE ( 'NONE', *, *, #10673, .T. ) ;
#12369=CARTESIAN_POINT ( 'NONE',  ( 0.000000000000000000, 0.000000000000000000, -30.00000000000000000 ) ) ;
#12370=AXIS2_PLACEMENT_3D ( 'NONE', #14841, #17890, #9444 ) ;
#12421=DIRECTION ( 'NONE',  ( -1.000000000000000000, 0.000000000000000000, 0.000000000000000000 ) ) ;
#12457=DIRECTION ( 'NONE',  ( -1.000000000000000000, 0.000000000000000000, 0.000000000000000000 ) ) ;
#12459=EDGE_CURVE ( 'NONE', #16430, #21087, #16677, .T. ) ;
#12461=FILL_AREA_STYLE ('',( #8970 ) ) ;
#12484=CARTESIAN_POINT ( 'NONE',  ( -24.63401512838747820, 0.000000000000000000, 77.51594804401857175 ) ) ;
#12496=DIRECTION ( 'NONE',  ( -0.000000000000000000, -0.000000000000000000, -1.000000000000000000 ) ) ;
#12558=DIRECTION ( 'NONE',  ( -1.000000000000000000, 0.000000000000000000, 0.000000000000000000 ) ) ;
#12564=( NAMED_UNIT ( * ) PLANE_ANGLE_UNIT ( ) SI_UNIT ( $, .RADIAN. ) );
#12567=ORIENTED_EDGE ( 'NONE', *, *, #21369, .T. ) ;
#12570=LINE ( 'NONE', #17969, #15231 ) ;
#12587=DIRECTION ( 'NONE',  ( -0.000000000000000000, -0.000000000000000000, -1.000000000000000000 ) ) ;
#12602=LINE ( 'NONE', #21030, #5828 ) ;
#12637=DIRECTION ( 'NONE',  ( 0.000000000000000000, 0.000000000000000000, -1.000000000000000000 ) ) ;
#12646=VERTEX_POINT ( 'NONE', #4805 ) ;
#12650=CIRCLE ( 'NONE', #12283, 3.000000000000002665 ) ;
#12656=CARTESIAN_POINT ( 'NONE',  ( 0.000000000000000000, 0.000000000000000000, -55.00000000000000000 ) ) ;
#12666=DIRECTION ( 'NONE',  ( 0.000000000000000000, 0.000000000000000000, 1.000000000000000000 ) ) ;
#12679=DIRECTION ( 'NONE',  ( -1.000000000000000000, 0.000000000000000000, 0.000000000000000000 ) ) ;
#12711=FACE_OUTER_BOUND ( 'NONE', #17568, .T. ) ;
#12715=CIRCLE ( 'NONE', #21677, 3.000000000000002665 ) ;
#12725=EDGE_CURVE ( 'NONE', #2304, #1564, #5027, .T. ) ;
#12759=CARTESIAN_POINT ( 'NONE',  ( 0.000000000000000000, 0.000000000000000000, -77.51594804401857175 ) ) ;
#12765=( GEOMETRIC_REPRESENTATION_CONTEXT ( 3 ) GLOBAL_UNCERTAINTY_ASSIGNED_CONTEXT ( ( #17775 ) ) GLOBAL_UNIT_ASSIGNED_CONTEXT ( ( #3556, #12564, #3993 ) ) REPRESENTATION_CONTEXT ( 'NONE', 'WORKASPACE' ) );
#12782=AXIS2_PLACEMENT_3D ( 'NONE', #18875, #20999, #6955 ) ;
#12791=DIRECTION ( 'NONE',  ( -1.000000000000000000, 0.000000000000000000, -0.000000000000000000 ) ) ;
#12803=VERTEX_POINT ( 'NONE', #18552 ) ;
#12815=CARTESIAN_POINT ( 'NONE',  ( 0.000000000000000000, 0.000000000000000000, 78.50000000000000000 ) ) ;
#12846=DIRECTION ( 'NONE',  ( 1.000000000000000000, -1.083936797661035110E-15, 0.000000000000000000 ) ) ;
#12847=ADVANCED_FACE ( 'NONE', ( #15294 ), #14192, .F. ) ;
#12883=CARTESIAN_POINT ( 'NONE',  ( 0.000000000000000000, 0.000000000000000000, 77.51594804401857175 ) ) ;
#12898=EDGE_CURVE ( 'NONE', #20089, #3205, #10579, .T. ) ;
#12908=EDGE_LOOP ( 'NONE', ( #11338, #18205, #12094, #16151 ) ) ;
#12926=CYLINDRICAL_SURFACE ( 'NONE', #15592, 20.99999999999999645 ) ;
#12966=DIRECTION ( 'NONE',  ( -1.000000000000000000, 0.000000000000000000, 0.000000000000000000 ) ) ;
#12988=DIRECTION ( 'NONE',  ( -1.000000000000000000, 0.000000000000000000, 0.000000000000000000 ) ) ;
#12989=DIRECTION ( 'NONE',  ( 0.000000000000000000, 0.000000000000000000, 1.000000000000000000 ) ) ;
#13000=VERTEX_POINT ( 'NONE', #1988 ) ;
#13009=TOROIDAL_SURFACE ( 'NONE', #7621, 22.63401512838748175, 3.000000000000002665 ) ;
#13023=ORIENTED_EDGE ( 'NONE', *, *, #12898, .F. ) ;
#13038=CARTESIAN_POINT ( 'NONE',  ( 1.526556658859590243E-13, -21.00000000000000000, 75.00000000000000000 ) ) ;
#13052=SHAPE_REPRESENTATION ( 'bottom housing_bottom housing', ( #6677 ), #8455 ) ;
#13058=FACE_OUTER_BOUND ( 'NONE', #21179, .T. ) ;
#13106=LINE ( 'NONE', #11306, #73 ) ;
#13120=DIRECTION ( 'NONE',  ( -1.000000000000000000, 0.000000000000000000, 0.000000000000000000 ) ) ;
#13126=EDGE_CURVE ( 'NONE', #22217, #12646, #208, .T. ) ;
#13128=FACE_OUTER_BOUND ( 'NONE', #19469, .T. ) ;
#13138=ORIENTED_EDGE ( 'NONE', *, *, #14186, .T. ) ;
#13154=CYLINDRICAL_SURFACE ( 'NONE', #471, 17.50000000000000711 ) ;
#13178=DIRECTION ( 'NONE',  ( 1.000000000000000000, 0.000000000000000000, 0.000000000000000000 ) ) ;
#13179=ADVANCED_FACE ( 'NONE', ( #6841 ), #3056, .F. ) ;
#13228=DIRECTION ( 'NONE',  ( 0.000000000000000000, 0.000000000000000000, -1.000000000000000000 ) ) ;
#13257=CARTESIAN_POINT ( 'NONE',  ( -25.00000000000000000, 0.000000000000000000, 75.00000000000000000 ) ) ;
#13261=CARTESIAN_POINT ( 'NONE',  ( -17.50000000000000711, 0.000000000000000000, -60.00000000000000000 ) ) ;
#13298=DIRECTION ( 'NONE',  ( 0.000000000000000000, 0.000000000000000000, 1.000000000000000000 ) ) ;
#13323=DIRECTION ( 'NONE',  ( 1.000000000000000000, 6.982962677686266711E-15, 0.000000000000000000 ) ) ;
#13332=ORIENTED_EDGE ( 'NONE', *, *, #15276, .T. ) ;
#13336=DIRECTION ( 'NONE',  ( -0.000000000000000000, -0.000000000000000000, -1.000000000000000000 ) ) ;
#13370=DIRECTION ( 'NONE',  ( 0.000000000000000000, 0.000000000000000000, -1.000000000000000000 ) ) ;
#13371=CIRCLE ( 'NONE', #9773, 23.00000000000000000 ) ;
#13394=DIRECTION ( 'NONE',  ( 0.000000000000000000, 0.000000000000000000, -1.000000000000000000 ) ) ;
#13418=VECTOR ( 'NONE', #11901, 1000.000000000000000 ) ;
#13430=SURFACE_STYLE_USAGE ( .BOTH. , #11854 ) ;
#13437=CIRCLE ( 'NONE', #8777, 20.99999999999999645 ) ;
#13439=CYLINDRICAL_SURFACE ( 'NONE', #10838, 17.50000000000000711 ) ;
#13452=DIRECTION ( 'NONE',  ( -0.000000000000000000, -0.000000000000000000, -1.000000000000000000 ) ) ;
#13463=ORIENTED_EDGE ( 'NONE', *, *, #4223, .T. ) ;
#13469=ORIENTED_EDGE ( 'NONE', *, *, #19326, .F. ) ;
#13491=AXIS2_PLACEMENT_3D ( 'NONE', #20914, #10465, #10695 ) ;
#13508=CIRCLE ( 'NONE', #19596, 21.63401512838748175 ) ;
#13528=EDGE_CURVE ( 'NONE', #11, #21087, #740, .T. ) ;
#13529=CIRCLE ( 'NONE', #8857, 3.000000000000002665 ) ;
#13542=ORIENTED_EDGE ( 'NONE', *, *, #16056, .F. ) ;
#13572=DIRECTION ( 'NONE',  ( 1.000000000000000000, 0.000000000000000000, 0.000000000000000000 ) ) ;
#13587=DIRECTION ( 'NONE',  ( 0.000000000000000000, 0.000000000000000000, 1.000000000000000000 ) ) ;
#13588=VERTEX_POINT ( 'NONE', #2969 ) ;
#13593=CARTESIAN_POINT ( 'NONE',  ( 0.000000000000000000, 0.000000000000000000, -77.51594804401857175 ) ) ;
#13599=DIRECTION ( 'NONE',  ( -0.000000000000000000, -0.000000000000000000, 1.000000000000000000 ) ) ;
#13613=ORIENTED_EDGE ( 'NONE', *, *, #65, .F. ) ;
#13616=ORIENTED_EDGE ( 'NONE', *, *, #17888, .T. ) ;
#13644=CARTESIAN_POINT ( 'NONE',  ( 0.000000000000000000, 0.000000000000000000, -77.51594804401857175 ) ) ;
#13698=EDGE_CURVE ( 'NONE', #18856, #5014, #6356, .T. ) ;
#13756=CARTESIAN_POINT ( 'NONE',  ( 0.000000000000000000, -17.50000000000000711, -60.00000000000000000 ) ) ;
#13762=CIRCLE ( 'NONE', #1173, 3.000000000000002665 ) ;
#13771=DIRECTION ( 'NONE',  ( -0.000000000000000000, -0.000000000000000000, -1.000000000000000000 ) ) ;
#13778=AXIS2_PLACEMENT_3D ( 'NONE', #13644, #4851, #5071 ) ;
#13788=ORIENTED_EDGE ( 'NONE', *, *, #4940, .F. ) ;
#13796=AXIS2_PLACEMENT_3D ( 'NONE', #8785, #15645, #227 ) ;
#13798=AXIS2_PLACEMENT_3D ( 'NONE', #5244, #11795, #12126 ) ;
#13811=VERTEX_POINT ( 'NONE', #6467 ) ;
#13815=DIRECTION ( 'NONE',  ( -1.000000000000000000, -0.000000000000000000, -0.000000000000000000 ) ) ;
#13825=DIRECTION ( 'NONE',  ( 0.000000000000000000, 1.000000000000000000, -0.000000000000000000 ) ) ;
#13826=EDGE_CURVE ( 'NONE', #68, #10234, #22075, .T. ) ;
#13837=VERTEX_POINT ( 'NONE', #1184 ) ;
#13857=PLANE ( 'NONE',  #11956 ) ;
#13869=VECTOR ( 'NONE', #15430, 1000.000000000000000 ) ;
#13897=VECTOR ( 'NONE', #16668, 1000.000000000000000 ) ;
#13899=EDGE_CURVE ( 'NONE', #14126, #15384, #6701, .T. ) ;
#13925=ORIENTED_EDGE ( 'NONE', *, *, #18240, .T. ) ;
#13980=DIRECTION ( 'NONE',  ( -0.000000000000000000, -0.000000000000000000, -1.000000000000000000 ) ) ;
#13982=DIRECTION ( 'NONE',  ( -0.000000000000000000, -0.000000000000000000, -1.000000000000000000 ) ) ;
#13987=ORIENTED_EDGE ( 'NONE', *, *, #14886, .F. ) ;
#14017=DIRECTION ( 'NONE',  ( -1.083936797661035110E-15, -1.000000000000000000, 0.000000000000000000 ) ) ;
#14058=ORIENTED_EDGE ( 'NONE', *, *, #9702, .F. ) ;
#14064=DIRECTION ( 'NONE',  ( -0.000000000000000000, -0.000000000000000000, 1.000000000000000000 ) ) ;
#14070=EDGE_CURVE ( 'NONE', #19932, #14271, #4474, .T. ) ;
#14076=FACE_OUTER_BOUND ( 'NONE', #2500, .T. ) ;
#14077=FACE_OUTER_BOUND ( 'NONE', #9756, .T. ) ;
#14083=ORIENTED_EDGE ( 'NONE', *, *, #6929, .F. ) ;
#14085=ORIENTED_EDGE ( 'NONE', *, *, #11000, .T. ) ;
#14126=VERTEX_POINT ( 'NONE', #20969 ) ;
#14152=CARTESIAN_POINT ( 'NONE',  ( 0.000000000000000000, 20.99999999999999645, 69.99999999999998579 ) ) ;
#14159=ORIENTED_EDGE ( 'NONE', *, *, #13899, .T. ) ;
#14162=CIRCLE ( 'NONE', #4778, 17.50000000000000711 ) ;
#14178=DIRECTION ( 'NONE',  ( -1.000000000000000000, 0.000000000000000000, 0.000000000000000000 ) ) ;
#14179=TOROIDAL_SURFACE ( 'NONE', #6607, 24.63401512838747820, 3.000000000000000888 ) ;
#14180=ORIENTED_EDGE ( 'NONE', *, *, #9431, .T. ) ;
#14186=EDGE_CURVE ( 'NONE', #15384, #1564, #10244, .T. ) ;
#14192=TOROIDAL_SURFACE ( 'NONE', #7361, 24.63401512838747820, 3.000000000000000888 ) ;
#14193=DIRECTION ( 'NONE',  ( 1.000000000000000000, 0.000000000000000000, 0.000000000000000000 ) ) ;
#14201=ORIENTED_EDGE ( 'NONE', *, *, #12149, .F. ) ;
#14218=CARTESIAN_POINT ( 'NONE',  ( 1.387778780781445676E-13, -19.79999999999999716, -78.50000000000000000 ) ) ;
#14219=EDGE_CURVE ( 'NONE', #1604, #22159, #1845, .T. ) ;
#14227=AXIS2_PLACEMENT_3D ( 'NONE', #3588, #10908, #15869 ) ;
#14228=CIRCLE ( 'NONE', #2346, 21.63401512838748175 ) ;
#14271=VERTEX_POINT ( 'NONE', #20745 ) ;
#14274=LINE ( 'NONE', #417, #6588 ) ;
#14283=ORIENTED_EDGE ( 'NONE', *, *, #13899, .F. ) ;
#14290=VERTEX_POINT ( 'NONE', #12208 ) ;
#14298=CYLINDRICAL_SURFACE ( 'NONE', #10912, 20.99999999999999645 ) ;
#14301=DIRECTION ( 'NONE',  ( -0.000000000000000000, -0.000000000000000000, 1.000000000000000000 ) ) ;
#14308=ORIENTED_EDGE ( 'NONE', *, *, #17232, .F. ) ;
#14343=AXIS2_PLACEMENT_3D ( 'NONE', #18998, #12587, #4017 ) ;
#14361=ORIENTED_EDGE ( 'NONE', *, *, #2596, .F. ) ;
#14366=FACE_OUTER_BOUND ( 'NONE', #22036, .T. ) ;
#14370=DIRECTION ( 'NONE',  ( -1.000000000000000000, 0.000000000000000000, 0.000000000000000000 ) ) ;
#14378=LINE ( 'NONE', #21106, #2626 ) ;
#14387=DIRECTION ( 'NONE',  ( 1.000000000000000000, 6.982962677686266711E-15, 0.000000000000000000 ) ) ;
#14390=EDGE_LOOP ( 'NONE', ( #14201, #10958, #1336, #19783 ) ) ;
#14442=DIRECTION ( 'NONE',  ( 0.000000000000000000, 6.938893903907222461E-16, 1.000000000000000000 ) ) ;
#14446=VECTOR ( 'NONE', #1503, 1000.000000000000000 ) ;
#14451=ORIENTED_EDGE ( 'NONE', *, *, #8739, .F. ) ;
#14470=CARTESIAN_POINT ( 'NONE',  ( 0.000000000000000000, -23.00000000000000000, 75.00000000000000000 ) ) ;
#14472=AXIS2_PLACEMENT_3D ( 'NONE', #3695, #558, #10580 ) ;
#14490=CIRCLE ( 'NONE', #4057, 3.000000000000002665 ) ;
#14506=FACE_OUTER_BOUND ( 'NONE', #7584, .T. ) ;
#14509=AXIS2_PLACEMENT_3D ( 'NONE', #12815, #9550, #3829 ) ;
#14516=CARTESIAN_POINT ( 'NONE',  ( 0.000000000000000000, 0.000000000000000000, -60.00000000000001421 ) ) ;
#14525=CIRCLE ( 'NONE', #16631, 23.00000000000000000 ) ;
#14543=DIRECTION ( 'NONE',  ( 1.000000000000000000, 0.000000000000000000, 0.000000000000000000 ) ) ;
#14558=CYLINDRICAL_SURFACE ( 'NONE', #5493, 20.99999999999999645 ) ;
#14579=ORIENTED_EDGE ( 'NONE', *, *, #10780, .T. ) ;
#14625=ADVANCED_FACE ( 'NONE', ( #8119 ), #16696, .T. ) ;
#14639=VERTEX_POINT ( 'NONE', #2396 ) ;
#14675=ORIENTED_EDGE ( 'NONE', *, *, #12898, .T. ) ;
#14682=CARTESIAN_POINT ( 'NONE',  ( 0.000000000000000000, 0.000000000000000000, -69.99999999999998579 ) ) ;
#14692=FACE_OUTER_BOUND ( 'NONE', #5114, .T. ) ;
#14795=CARTESIAN_POINT ( 'NONE',  ( 0.000000000000000000, 0.000000000000000000, -55.00000000000000000 ) ) ;
#14796=CARTESIAN_POINT ( 'NONE',  ( 0.000000000000000000, 24.63401512838747820, 77.51594804401857175 ) ) ;
#14821=ORIENTED_EDGE ( 'NONE', *, *, #17961, .T. ) ;
#14833=DIRECTION ( 'NONE',  ( -1.000000000000000000, 0.000000000000000000, 0.000000000000000000 ) ) ;
#14836=VECTOR ( 'NONE', #16727, 1000.000000000000000 ) ;
#14841=CARTESIAN_POINT ( 'NONE',  ( 0.000000000000000000, 0.000000000000000000, 78.50000000000000000 ) ) ;
#14886=EDGE_CURVE ( 'NONE', #19977, #17437, #9520, .T. ) ;
#14952=CARTESIAN_POINT ( 'NONE',  ( 0.000000000000000000, -17.50000000000000711, -55.00000000000000000 ) ) ;
#14962=DIRECTION ( 'NONE',  ( 0.000000000000000000, 0.000000000000000000, -1.000000000000000000 ) ) ;
#15007=ORIENTED_EDGE ( 'NONE', *, *, #11475, .T. ) ;
#15014=CARTESIAN_POINT ( 'NONE',  ( -23.00000000000000355, 0.000000000000000000, -75.00000000000000000 ) ) ;
#15037=DIRECTION ( 'NONE',  ( -0.000000000000000000, -0.000000000000000000, -1.000000000000000000 ) ) ;
#15051=VECTOR ( 'NONE', #1650, 1000.000000000000000 ) ;
#15059=CARTESIAN_POINT ( 'NONE',  ( 0.000000000000000000, 22.63401512838748175, 77.51594804401857175 ) ) ;
#15077=EDGE_CURVE ( 'NONE', #11287, #22159, #15998, .T. ) ;
#15112=DIRECTION ( 'NONE',  ( 1.000000000000000000, 0.000000000000000000, 0.000000000000000000 ) ) ;
#15119=ORIENTED_EDGE ( 'NONE', *, *, #4223, .F. ) ;
#15126=CARTESIAN_POINT ( 'NONE',  ( -21.80000000000000071, 0.000000000000000000, 78.50000000000000000 ) ) ;
#15133=DIRECTION ( 'NONE',  ( -1.000000000000000000, 0.000000000000000000, 0.000000000000000000 ) ) ;
#15134=DIRECTION ( 'NONE',  ( 1.000000000000000000, 0.000000000000000000, -0.000000000000000000 ) ) ;
#15143=ORIENTED_EDGE ( 'NONE', *, *, #6802, .T. ) ;
#15198=EDGE_CURVE ( 'NONE', #7178, #2436, #1355, .T. ) ;
#15231=VECTOR ( 'NONE', #19415, 1000.000000000000000 ) ;
#15264=VECTOR ( 'NONE', #13452, 1000.000000000000000 ) ;
#15276=EDGE_CURVE ( 'NONE', #17859, #8719, #3143, .T. ) ;
#15280=CARTESIAN_POINT ( 'NONE',  ( 1.455845656607146809E-13, -21.63401512838747820, 77.51594804401857175 ) ) ;
#15284=DIRECTION ( 'NONE',  ( 0.000000000000000000, 0.000000000000000000, 1.000000000000000000 ) ) ;
#15292=CARTESIAN_POINT ( 'NONE',  ( 0.000000000000000000, -17.50000000000000711, -24.99999999999999645 ) ) ;
#15294=FACE_OUTER_BOUND ( 'NONE', #5320, .T. ) ;
#15302=ORIENTED_EDGE ( 'NONE', *, *, #15761, .T. ) ;
#15345=ORIENTED_EDGE ( 'NONE', *, *, #16713, .F. ) ;
#15384=VERTEX_POINT ( 'NONE', #22171 ) ;
#15406=CARTESIAN_POINT ( 'NONE',  ( -23.00000000000000000, 0.000000000000000000, 69.99999999999998579 ) ) ;
#15408=CIRCLE ( 'NONE', #8582, 23.00000000000000000 ) ;
#15430=DIRECTION ( 'NONE',  ( -6.982962677686266711E-15, 1.000000000000000000, 0.000000000000000000 ) ) ;
#15523=EDGE_CURVE ( 'NONE', #20366, #2937, #8566, .T. ) ;
#15525=CIRCLE ( 'NONE', #20165, 3.000000000000002665 ) ;
#15527=AXIS2_PLACEMENT_3D ( 'NONE', #4758, #9957, #1392 ) ;
#15533=DIRECTION ( 'NONE',  ( -1.000000000000000000, 0.000000000000000000, 0.000000000000000000 ) ) ;
#15578=EDGE_CURVE ( 'NONE', #8719, #20147, #18163, .T. ) ;
#15583=ORIENTED_EDGE ( 'NONE', *, *, #7373, .T. ) ;
#15592=AXIS2_PLACEMENT_3D ( 'NONE', #880, #16195, #4351 ) ;
#15594=AXIS2_PLACEMENT_3D ( 'NONE', #1873, #13825, #15733 ) ;
#15596=DIRECTION ( 'NONE',  ( -0.000000000000000000, -1.000000000000000000, -0.000000000000000000 ) ) ;
#15601=ORIENTED_EDGE ( 'NONE', *, *, #21369, .F. ) ;
#15606=CARTESIAN_POINT ( 'NONE',  ( 1.387778780781445676E-13, -19.79999999999999716, 78.50000000000000000 ) ) ;
#15624=ADVANCED_FACE ( 'NONE', ( #5721 ), #17782, .T. ) ;
#15645=DIRECTION ( 'NONE',  ( 0.000000000000000000, 0.000000000000000000, -1.000000000000000000 ) ) ;
#15664=DIRECTION ( 'NONE',  ( 1.000000000000000000, 6.982962677686266711E-15, 0.000000000000000000 ) ) ;
#15733=DIRECTION ( 'NONE',  ( 0.000000000000000000, 0.000000000000000000, 1.000000000000000000 ) ) ;
#15745=ADVANCED_FACE ( 'NONE', ( #7210 ), #21134, .F. ) ;
#15751=CARTESIAN_POINT ( 'NONE',  ( 0.000000000000000000, 0.000000000000000000, 75.00000000000000000 ) ) ;
#15752=VERTEX_POINT ( 'NONE', #20696 ) ;
#15761=EDGE_CURVE ( 'NONE', #10560, #7254, #901, .T. ) ;
#15779=CIRCLE ( 'NONE', #3523, 23.00000000000000000 ) ;
#15792=DIRECTION ( 'NONE',  ( 1.000000000000000000, 0.000000000000000000, 0.000000000000000000 ) ) ;
#15809=VERTEX_POINT ( 'NONE', #19011 ) ;
#15819=DIRECTION ( 'NONE',  ( -1.000000000000000000, 0.000000000000000000, 0.000000000000000000 ) ) ;
#15828=ORIENTED_EDGE ( 'NONE', *, *, #17961, .F. ) ;
#15869=DIRECTION ( 'NONE',  ( -1.000000000000000000, 0.000000000000000000, 0.000000000000000000 ) ) ;
#15870=DIRECTION ( 'NONE',  ( -1.000000000000000000, 0.000000000000000000, 0.000000000000000000 ) ) ;
#15885=CARTESIAN_POINT ( 'NONE',  ( -24.63401512838747820, 0.000000000000000000, 77.51594804401857175 ) ) ;
#15887=AXIS2_PLACEMENT_3D ( 'NONE', #12883, #4424, #21638 ) ;
#15914=AXIS2_PLACEMENT_3D ( 'NONE', #1692, #18580, #6758 ) ;
#15952=DIRECTION ( 'NONE',  ( 0.000000000000000000, 0.000000000000000000, -1.000000000000000000 ) ) ;
#15991=EDGE_CURVE ( 'NONE', #10560, #16621, #10616, .T. ) ;
#15998=CIRCLE ( 'NONE', #6279, 3.000000000000002665 ) ;
#16000=COLOUR_RGB ( '', 0.08235294, 0.09019608, 0.10196078) ;
#16018=AXIS2_PLACEMENT_3D ( 'NONE', #10968, #8955, #15819 ) ;
#16025=ADVANCED_FACE ( 'NONE', ( #14076 ), #9005, .T. ) ;
#16028=ORIENTED_EDGE ( 'NONE', *, *, #10351, .F. ) ;
#16056=EDGE_CURVE ( 'NONE', #7254, #20783, #16714, .T. ) ;
#16062=EDGE_LOOP ( 'NONE', ( #10318, #7508, #13138, #8772, #19620, #5674 ) ) ;
#16118=LINE ( 'NONE', #11160, #7427 ) ;
#16127=DIRECTION ( 'NONE',  ( -1.000000000000000000, 0.000000000000000000, 0.000000000000000000 ) ) ;
#16137=ORIENTED_EDGE ( 'NONE', *, *, #19244, .T. ) ;
#16150=ORIENTED_EDGE ( 'NONE', *, *, #5782, .T. ) ;
#16151=ORIENTED_EDGE ( 'NONE', *, *, #17798, .F. ) ;
#16155=ADVANCED_FACE ( 'NONE', ( #12711 ), #3043, .F. ) ;
#16157=CARTESIAN_POINT ( 'NONE',  ( 0.000000000000000000, 0.000000000000000000, -24.99999999999999645 ) ) ;
#16158=CARTESIAN_POINT ( 'NONE',  ( -21.63401512838747820, 0.000000000000000000, -77.51594804401857175 ) ) ;
#16166=ORIENTED_EDGE ( 'NONE', *, *, #12459, .F. ) ;
#16169=FACE_OUTER_BOUND ( 'NONE', #16614, .T. ) ;
#16180=VERTEX_POINT ( 'NONE', #19999 ) ;
#16195=DIRECTION ( 'NONE',  ( 0.000000000000000000, 0.000000000000000000, -1.000000000000000000 ) ) ;
#16226=DIRECTION ( 'NONE',  ( 0.000000000000000000, 0.000000000000000000, 1.000000000000000000 ) ) ;
#16271=ORIENTED_EDGE ( 'NONE', *, *, #8163, .T. ) ;
#16292=CARTESIAN_POINT ( 'NONE',  ( 0.000000000000000000, -17.50000000000000711, -55.00000000000000000 ) ) ;
#16293=ORIENTED_EDGE ( 'NONE', *, *, #15077, .T. ) ;
#16312=CIRCLE ( 'NONE', #2993, 3.000000000000002665 ) ;
#16324=DIRECTION ( 'NONE',  ( 0.000000000000000000, 0.000000000000000000, 1.000000000000000000 ) ) ;
#16328=VECTOR ( 'NONE', #10331, 1000.000000000000000 ) ;
#16330=DIRECTION ( 'NONE',  ( -1.000000000000000000, -6.982962677686266711E-15, -0.000000000000000000 ) ) ;
#16336=LINE ( 'NONE', #9259, #9588 ) ;
#16430=VERTEX_POINT ( 'NONE', #13038 ) ;
#16451=LINE ( 'NONE', #11053, #10292 ) ;
#16460=PLANE ( 'NONE',  #18801 ) ;
#16473=DIRECTION ( 'NONE',  ( 0.000000000000000000, 0.000000000000000000, -1.000000000000000000 ) ) ;
#16505=EDGE_CURVE ( 'NONE', #3205, #20901, #3122, .T. ) ;
#16511=EDGE_LOOP ( 'NONE', ( #13987, #17335, #2809, #7038 ) ) ;
#16533=VERTEX_POINT ( 'NONE', #15406 ) ;
#16548=FACE_OUTER_BOUND ( 'NONE', #21012, .T. ) ;
#16580=CARTESIAN_POINT ( 'NONE',  ( 0.000000000000000000, 17.50000000000000711, -55.00000000000000000 ) ) ;
#16599=ORIENTED_EDGE ( 'NONE', *, *, #9431, .F. ) ;
#16614=EDGE_LOOP ( 'NONE', ( #4813, #9643, #13332, #1985, #671, #11735 ) ) ;
#16621=VERTEX_POINT ( 'NONE', #8313 ) ;
#16631=AXIS2_PLACEMENT_3D ( 'NONE', #7786, #11265, #14543 ) ;
#16638=CARTESIAN_POINT ( 'NONE',  ( 0.000000000000000000, 0.000000000000000000, -77.51594804401857175 ) ) ;
#16639=DIRECTION ( 'NONE',  ( 0.000000000000000000, 1.000000000000000000, -0.000000000000000000 ) ) ;
#16668=DIRECTION ( 'NONE',  ( 4.845403715540889009E-30, -6.938893903907222461E-16, 1.000000000000000000 ) ) ;
#16677=CIRCLE ( 'NONE', #20616, 21.00000000000000000 ) ;
#16696=TOROIDAL_SURFACE ( 'NONE', #3025, 22.63401512838748175, 3.000000000000002665 ) ;
#16713=EDGE_CURVE ( 'NONE', #15809, #13837, #3898, .T. ) ;
#16714=CIRCLE ( 'NONE', #1627, 19.79999999999999716 ) ;
#16727=DIRECTION ( 'NONE',  ( 0.000000000000000000, -1.000000000000000000, 0.000000000000000000 ) ) ;
#16761=ORIENTED_EDGE ( 'NONE', *, *, #586, .F. ) ;
#16793=CARTESIAN_POINT ( 'NONE',  ( 0.000000000000000000, 0.000000000000000000, -24.99999999999999645 ) ) ;
#16808=LINE ( 'NONE', #10282, #5215 ) ;
#16840=VERTEX_POINT ( 'NONE', #2671 ) ;
#16861=AXIS2_PLACEMENT_3D ( 'NONE', #10787, #19104, #2333 ) ;
#16866=CARTESIAN_POINT ( 'NONE',  ( -22.63401512838748175, 0.000000000000000000, 77.51594804401857175 ) ) ;
#16890=CARTESIAN_POINT ( 'NONE',  ( -23.00000000000000000, 0.000000000000000000, -69.99999999999998579 ) ) ;
#16910=ORIENTED_EDGE ( 'NONE', *, *, #17351, .T. ) ;
#16938=VERTEX_POINT ( 'NONE', #20208 ) ;
#16969=AXIS2_PLACEMENT_3D ( 'NONE', #72, #13815, #20654 ) ;
#16970=CARTESIAN_POINT ( 'NONE',  ( 0.000000000000000000, 0.000000000000000000, 75.00000000000000000 ) ) ;
#16977=CIRCLE ( 'NONE', #4027, 17.50000000000000711 ) ;
#17003=DIRECTION ( 'NONE',  ( -0.000000000000000000, -1.000000000000000000, -0.000000000000000000 ) ) ;
#17009=AXIS2_PLACEMENT_3D ( 'NONE', #8204, #22028, #1220 ) ;
#17017=ORIENTED_EDGE ( 'NONE', *, *, #11475, .F. ) ;
#17052=ORIENTED_EDGE ( 'NONE', *, *, #12725, .T. ) ;
#17083=EDGE_CURVE ( 'NONE', #16180, #10560, #488, .T. ) ;
#17085=CARTESIAN_POINT ( 'NONE',  ( 0.000000000000000000, 17.50000000000000711, -24.99999999999999645 ) ) ;
#17102=ORIENTED_EDGE ( 'NONE', *, *, #20117, .F. ) ;
#17124=ORIENTED_EDGE ( 'NONE', *, *, #464, .F. ) ;
#17154=PRODUCT ( 'bottom housing_bottom housing', 'bottom housing_bottom housing', '', ( #21532 ) ) ;
#17214=CIRCLE ( 'NONE', #14343, 23.00000000000000000 ) ;
#17217=CARTESIAN_POINT ( 'NONE',  ( 0.000000000000000000, 0.000000000000000000, -75.00000000000000000 ) ) ;
#17232=EDGE_CURVE ( 'NONE', #12271, #4321, #10913, .T. ) ;
#17236=CARTESIAN_POINT ( 'NONE',  ( 1.317067778529001989E-13, -19.63401512838747820, -77.51594804401857175 ) ) ;
#17248=DIRECTION ( 'NONE',  ( 0.000000000000000000, 0.000000000000000000, -1.000000000000000000 ) ) ;
#17263=EDGE_CURVE ( 'NONE', #19544, #8365, #1662, .T. ) ;
#17277=DIRECTION ( 'NONE',  ( 1.000000000000000000, 0.000000000000000000, 0.000000000000000000 ) ) ;
#17294=SURFACE_SIDE_STYLE ('',( #18977 ) ) ;
#17315=FACE_OUTER_BOUND ( 'NONE', #5212, .T. ) ;
#17323=CIRCLE ( 'NONE', #2564, 3.000000000000002665 ) ;
#17335=ORIENTED_EDGE ( 'NONE', *, *, #17531, .F. ) ;
#17339=AXIS2_PLACEMENT_3D ( 'NONE', #10358, #2129, #15870 ) ;
#17343=FACE_OUTER_BOUND ( 'NONE', #19399, .T. ) ;
#17344=DIRECTION ( 'NONE',  ( 0.000000000000000000, 1.000000000000000000, -0.000000000000000000 ) ) ;
#17345=CARTESIAN_POINT ( 'NONE',  ( 0.000000000000000000, 19.79999999999999716, 78.50000000000000000 ) ) ;
#17351=EDGE_CURVE ( 'NONE', #16840, #17518, #3353, .T. ) ;
#17353=AXIS2_PLACEMENT_3D ( 'NONE', #21802, #15596, #6389 ) ;
#17359=DIRECTION ( 'NONE',  ( -1.000000000000000000, 0.000000000000000000, 0.000000000000000000 ) ) ;
#17368=TOROIDAL_SURFACE ( 'NONE', #11972, 22.63401512838748175, 3.000000000000002665 ) ;
#17389=AXIS2_PLACEMENT_3D ( 'NONE', #8418, #22135, #9761 ) ;
#17393=CARTESIAN_POINT ( 'NONE',  ( 1.665334536937734811E-13, -23.00000000000000000, -69.99999999999998579 ) ) ;
#17409=EDGE_CURVE ( 'NONE', #14126, #2304, #18453, .T. ) ;
#17412=SURFACE_STYLE_USAGE ( .BOTH. , #17294 ) ;
#17430=ORIENTED_EDGE ( 'NONE', *, *, #21540, .F. ) ;
#17437=VERTEX_POINT ( 'NONE', #1768 ) ;
#17477=CIRCLE ( 'NONE', #11371, 19.63401512838747820 ) ;
#17501=ORIENTED_EDGE ( 'NONE', *, *, #8739, .T. ) ;
#17518=VERTEX_POINT ( 'NONE', #15292 ) ;
#17531=EDGE_CURVE ( 'NONE', #68, #19977, #22042, .T. ) ;
#17536=CARTESIAN_POINT ( 'NONE',  ( 1.387778780781445676E-13, -19.79999999999999716, 78.50000000000000000 ) ) ;
#17566=ORIENTED_EDGE ( 'NONE', *, *, #473, .T. ) ;
#17568=EDGE_LOOP ( 'NONE', ( #7199, #13616, #7739, #4191 ) ) ;
#17574=AXIS2_PLACEMENT_3D ( 'NONE', #5787, #21421, #21199 ) ;
#17605=ORIENTED_EDGE ( 'NONE', *, *, #65, .T. ) ;
#17608=ORIENTED_EDGE ( 'NONE', *, *, #2239, .F. ) ;
#17609=DIRECTION ( 'NONE',  ( 0.000000000000000000, 0.000000000000000000, 1.000000000000000000 ) ) ;
#17624=CARTESIAN_POINT ( 'NONE',  ( 0.000000000000000000, 25.00000000000000000, 75.00000000000000000 ) ) ;
#17625=ORIENTED_EDGE ( 'NONE', *, *, #4400, .F. ) ;
#17641=EDGE_CURVE ( 'NONE', #13811, #21551, #14274, .T. ) ;
#17649=ORIENTED_EDGE ( 'NONE', *, *, #464, .T. ) ;
#17654=DIRECTION ( 'NONE',  ( -1.000000000000000000, 0.000000000000000000, 0.000000000000000000 ) ) ;
#17680=EDGE_CURVE ( 'NONE', #20147, #20901, #14162, .T. ) ;
#17685=CIRCLE ( 'NONE', #21611, 21.00000000000000000 ) ;
#17705=EDGE_CURVE ( 'NONE', #18856, #7596, #14378, .T. ) ;
#17716=ORIENTED_EDGE ( 'NONE', *, *, #17409, .F. ) ;
#17720=DIRECTION ( 'NONE',  ( -1.000000000000000000, 0.000000000000000000, 0.000000000000000000 ) ) ;
#17742=CARTESIAN_POINT ( 'NONE',  ( -23.00000000000000000, 0.000000000000000000, -55.00000000000000000 ) ) ;
#17748=ORIENTED_EDGE ( 'NONE', *, *, #20398, .F. ) ;
#17768=CARTESIAN_POINT ( 'NONE',  ( 0.000000000000000000, 0.000000000000000000, -78.50000000000000000 ) ) ;
#17773=VECTOR ( 'NONE', #19745, 1000.000000000000000 ) ;
#17775=UNCERTAINTY_MEASURE_WITH_UNIT (LENGTH_MEASURE( 1.000000000000000082E-05 ), #3556, 'distance_accuracy_value', 'NONE');
#17782=CYLINDRICAL_SURFACE ( 'NONE', #14227, 25.00000000000000000 ) ;
#17797=DIRECTION ( 'NONE',  ( 0.000000000000000000, 0.000000000000000000, -1.000000000000000000 ) ) ;
#17798=EDGE_CURVE ( 'NONE', #14639, #19932, #12570, .T. ) ;
#17805=EDGE_CURVE ( 'NONE', #2355, #12271, #5468, .T. ) ;
#17811=CARTESIAN_POINT ( 'NONE',  ( 1.526556658859590243E-13, -20.99999999999999645, 69.99999999999998579 ) ) ;
#17820=COLOUR_RGB ( '', 0.08235294, 0.09019608, 0.10196078) ;
#17838=CARTESIAN_POINT ( 'NONE',  ( 0.000000000000000000, -17.50000000000000711, -60.00000000000000000 ) ) ;
#17851=CARTESIAN_POINT ( 'NONE',  ( 0.000000000000000000, 0.000000000000000000, 75.00000000000000000 ) ) ;
#17859=VERTEX_POINT ( 'NONE', #10875 ) ;
#17874=ORIENTED_EDGE ( 'NONE', *, *, #2321, .T. ) ;
#17888=EDGE_CURVE ( 'NONE', #1956, #215, #7689, .T. ) ;
#17890=DIRECTION ( 'NONE',  ( -0.000000000000000000, -0.000000000000000000, -1.000000000000000000 ) ) ;
#17914=EDGE_LOOP ( 'NONE', ( #5145, #11606, #399, #18671 ) ) ;
#17922=CARTESIAN_POINT ( 'NONE',  ( 0.000000000000000000, -17.50000000000000711, -24.99999999999999645 ) ) ;
#17931=DIRECTION ( 'NONE',  ( -0.000000000000000000, -0.000000000000000000, -1.000000000000000000 ) ) ;
#17946=DIRECTION ( 'NONE',  ( 4.408728476930466911E-15, -1.000000000000000000, 0.000000000000000000 ) ) ;
#17961=EDGE_CURVE ( 'NONE', #11, #5879, #13437, .T. ) ;
#17969=CARTESIAN_POINT ( 'NONE',  ( 0.000000000000000000, 21.00000000000000000, -75.00000000000000000 ) ) ;
#17987=VERTEX_POINT ( 'NONE', #5798 ) ;
#18026=DIRECTION ( 'NONE',  ( 4.408728476930466911E-15, -1.000000000000000000, 0.000000000000000000 ) ) ;
#18028=CARTESIAN_POINT ( 'NONE',  ( 0.000000000000000000, 0.000000000000000000, 0.000000000000000000 ) ) ;
#18035=AXIS2_PLACEMENT_3D ( 'NONE', #2741, #13323, #6344 ) ;
#18040=ADVANCED_FACE ( 'NONE', ( #16169 ), #739, .T. ) ;
#18045=AXIS2_PLACEMENT_3D ( 'NONE', #2472, #16324, #7778 ) ;
#18070=ORIENTED_EDGE ( 'NONE', *, *, #4766, .F. ) ;
#18080=CIRCLE ( 'NONE', #17009, 19.79999999999999716 ) ;
#18100=VECTOR ( 'NONE', #8476, 1000.000000000000000 ) ;
#18101=AXIS2_PLACEMENT_3D ( 'NONE', #8537, #13599, #8757 ) ;
#18106=DIRECTION ( 'NONE',  ( -1.000000000000000000, 0.000000000000000000, 0.000000000000000000 ) ) ;
#18163=CIRCLE ( 'NONE', #7019, 17.50000000000000711 ) ;
#18201=ORIENTED_EDGE ( 'NONE', *, *, #861, .F. ) ;
#18205=ORIENTED_EDGE ( 'NONE', *, *, #704, .T. ) ;
#18208=ORIENTED_EDGE ( 'NONE', *, *, #15523, .F. ) ;
#18214=EDGE_CURVE ( 'NONE', #1152, #21209, #14525, .T. ) ;
#18231=EDGE_LOOP ( 'NONE', ( #18970, #11140, #5487, #6822, #10339, #17124 ) ) ;
#18239=FACE_OUTER_BOUND ( 'NONE', #1560, .T. ) ;
#18240=EDGE_CURVE ( 'NONE', #13837, #3651, #13762, .T. ) ;
#18246=CARTESIAN_POINT ( 'NONE',  ( 0.000000000000000000, 0.000000000000000000, -69.99999999999998579 ) ) ;
#18247=VERTEX_POINT ( 'NONE', #21379 ) ;
#18260=FACE_OUTER_BOUND ( 'NONE', #4858, .T. ) ;
#18268=ORIENTED_EDGE ( 'NONE', *, *, #5782, .F. ) ;
#18276=CARTESIAN_POINT ( 'NONE',  ( 0.000000000000000000, 17.50000000000000711, -55.00000000000000000 ) ) ;
#18290=AXIS2_PLACEMENT_3D ( 'NONE', #15751, #1891, #17654 ) ;
#18294=ORIENTED_EDGE ( 'NONE', *, *, #13698, .T. ) ;
#18308=ORIENTED_EDGE ( 'NONE', *, *, #5288, .F. ) ;
#18329=CARTESIAN_POINT ( 'NONE',  ( 0.000000000000000000, -23.00000000000000000, 75.00000000000000000 ) ) ;
#18374=EDGE_LOOP ( 'NONE', ( #8995, #9538, #7440, #3344 ) ) ;
#18382=CARTESIAN_POINT ( 'NONE',  ( -21.00000000000000000, 0.000000000000000000, 75.00000000000000000 ) ) ;
#18391=DIRECTION ( 'NONE',  ( 0.000000000000000000, 0.000000000000000000, -1.000000000000000000 ) ) ;
#18401=AXIS2_PLACEMENT_3D ( 'NONE', #14796, #15134, #12989 ) ;
#18411=DIRECTION ( 'NONE',  ( 1.000000000000000000, 0.000000000000000000, 0.000000000000000000 ) ) ;
#18412=AXIS2_PLACEMENT_3D ( 'NONE', #1865, #8746, #19079 ) ;
#18453=CIRCLE ( 'NONE', #1570, 25.00000000000000000 ) ;
#18477=ORIENTED_EDGE ( 'NONE', *, *, #7604, .F. ) ;
#18481=DIRECTION ( 'NONE',  ( -1.000000000000000000, 0.000000000000000000, 0.000000000000000000 ) ) ;
#18487=ADVANCED_FACE ( 'NONE', ( #16548 ), #21711, .T. ) ;
#18501=VECTOR ( 'NONE', #14017, 1000.000000000000000 ) ;
#18507=DIRECTION ( 'NONE',  ( 0.000000000000000000, 0.000000000000000000, -1.000000000000000000 ) ) ;
#18527=CARTESIAN_POINT ( 'NONE',  ( 0.000000000000000000, 23.00000000000000000, 69.99999999999998579 ) ) ;
#18537=CIRCLE ( 'NONE', #19941, 20.99999999999999645 ) ;
#18552=CARTESIAN_POINT ( 'NONE',  ( -23.00000000000000000, 0.000000000000000000, -60.00000000000000000 ) ) ;
#18556=CARTESIAN_POINT ( 'NONE',  ( 0.000000000000000000, -17.50000000000000711, -55.00000000000000000 ) ) ;
#18580=DIRECTION ( 'NONE',  ( 0.000000000000000000, 0.000000000000000000, -1.000000000000000000 ) ) ;
#18591=ORIENTED_EDGE ( 'NONE', *, *, #20425, .T. ) ;
#18602=EDGE_CURVE ( 'NONE', #20426, #14639, #3668, .T. ) ;
#18646=ADVANCED_FACE ( 'NONE', ( #6867 ), #8337, .T. ) ;
#18671=ORIENTED_EDGE ( 'NONE', *, *, #20887, .T. ) ;
#18689=DIRECTION ( 'NONE',  ( -1.000000000000000000, -0.000000000000000000, -0.000000000000000000 ) ) ;
#18705=DIRECTION ( 'NONE',  ( 0.000000000000000000, 0.000000000000000000, -1.000000000000000000 ) ) ;
#18751=LINE ( 'NONE', #1313, #12169 ) ;
#18756=DIRECTION ( 'NONE',  ( -0.000000000000000000, -0.000000000000000000, -1.000000000000000000 ) ) ;
#18764=AXIS2_PLACEMENT_3D ( 'NONE', #6010, #12666, #21304 ) ;
#18768=CARTESIAN_POINT ( 'NONE',  ( 0.000000000000000000, 0.000000000000000000, 77.51594804401857175 ) ) ;
#18801=AXIS2_PLACEMENT_3D ( 'NONE', #16793, #9931, #6429 ) ;
#18833=AXIS2_PLACEMENT_3D ( 'NONE', #15059, #7967, #2879 ) ;
#18856=VERTEX_POINT ( 'NONE', #3030 ) ;
#18861=DIRECTION ( 'NONE',  ( 0.000000000000000000, 0.000000000000000000, -1.000000000000000000 ) ) ;
#18875=CARTESIAN_POINT ( 'NONE',  ( 0.000000000000000000, 0.000000000000000000, -30.00000000000000000 ) ) ;
#18886=VERTEX_POINT ( 'NONE', #16890 ) ;
#18892=CARTESIAN_POINT ( 'NONE',  ( 1.455845656607146809E-13, -21.63401512838747820, -77.51594804401857175 ) ) ;
#18912=EDGE_LOOP ( 'NONE', ( #17874, #3801, #18208, #17102, #13542, #15143 ) ) ;
#18935=FILL_AREA_STYLE_COLOUR ( '', #17820 ) ;
#18960=LINE ( 'NONE', #8095, #6569 ) ;
#18970=ORIENTED_EDGE ( 'NONE', *, *, #3485, .F. ) ;
#18973=DIRECTION ( 'NONE',  ( 0.000000000000000000, 0.000000000000000000, -1.000000000000000000 ) ) ;
#18977=SURFACE_STYLE_FILL_AREA ( #12461 ) ;
#18996=ORIENTED_EDGE ( 'NONE', *, *, #3893, .T. ) ;
#18998=CARTESIAN_POINT ( 'NONE',  ( 0.000000000000000000, 0.000000000000000000, 75.00000000000000000 ) ) ;
#19011=CARTESIAN_POINT ( 'NONE',  ( 1.387778780781445676E-13, -19.79999999999999716, 78.50000000000000000 ) ) ;
#19012=DIRECTION ( 'NONE',  ( 0.000000000000000000, 0.000000000000000000, 1.000000000000000000 ) ) ;
#19041=CARTESIAN_POINT ( 'NONE',  ( 0.000000000000000000, 0.000000000000000000, 77.51594804401857175 ) ) ;
#19047=EDGE_CURVE ( 'NONE', #7303, #22217, #12602, .T. ) ;
#19079=DIRECTION ( 'NONE',  ( -1.000000000000000000, 0.000000000000000000, 0.000000000000000000 ) ) ;
#19104=DIRECTION ( 'NONE',  ( -0.000000000000000000, -0.000000000000000000, -1.000000000000000000 ) ) ;
#19132=CARTESIAN_POINT ( 'NONE',  ( 0.000000000000000000, 0.000000000000000000, -77.51594804401857175 ) ) ;
#19189=PLANE ( 'NONE',  #1377 ) ;
#19190=DIRECTION ( 'NONE',  ( -0.000000000000000000, -0.000000000000000000, -1.000000000000000000 ) ) ;
#19203=DIRECTION ( 'NONE',  ( -0.000000000000000000, -0.000000000000000000, -1.000000000000000000 ) ) ;
#19206=DIRECTION ( 'NONE',  ( 6.982962677686266711E-15, -1.000000000000000000, 0.000000000000000000 ) ) ;
#19213=ORIENTED_EDGE ( 'NONE', *, *, #18602, .T. ) ;
#19232=CARTESIAN_POINT ( 'NONE',  ( 0.000000000000000000, 0.000000000000000000, -77.51594804401857175 ) ) ;
#19244=EDGE_CURVE ( 'NONE', #20783, #16621, #1878, .T. ) ;
#19251=FACE_OUTER_BOUND ( 'NONE', #1196, .T. ) ;
#19275=TOROIDAL_SURFACE ( 'NONE', #4898, 22.63401512838748175, 3.000000000000002665 ) ;
#19277=ADVANCED_FACE ( 'NONE', ( #14077 ), #7434, .F. ) ;
#19296=EDGE_LOOP ( 'NONE', ( #14083, #14579, #14361, #17608 ) ) ;
#19302=ORIENTED_EDGE ( 'NONE', *, *, #15198, .T. ) ;
#19325=ORIENTED_EDGE ( 'NONE', *, *, #14070, .T. ) ;
#19326=EDGE_CURVE ( 'NONE', #21555, #10013, #458, .T. ) ;
#19331=CARTESIAN_POINT ( 'NONE',  ( -25.00000000000000000, 0.000000000000000000, 75.00000000000000000 ) ) ;
#19349=ORIENTED_EDGE ( 'NONE', *, *, #13826, .T. ) ;
#19351=VERTEX_POINT ( 'NONE', #8670 ) ;
#19386=ORIENTED_EDGE ( 'NONE', *, *, #6802, .F. ) ;
#19399=EDGE_LOOP ( 'NONE', ( #2463, #16910, #22066, #23 ) ) ;
#19405=CARTESIAN_POINT ( 'NONE',  ( -19.79999999999999716, 0.000000000000000000, 78.50000000000000000 ) ) ;
#19415=DIRECTION ( 'NONE',  ( -0.000000000000000000, 6.938893903907222461E-16, -1.000000000000000000 ) ) ;
#19426=EDGE_CURVE ( 'NONE', #7596, #11, #1529, .T. ) ;
#19432=CYLINDRICAL_SURFACE ( 'NONE', #18290, 23.00000000000000000 ) ;
#19433=ORIENTED_EDGE ( 'NONE', *, *, #1141, .F. ) ;
#19467=CIRCLE ( 'NONE', #18412, 23.00000000000000000 ) ;
#19469=EDGE_LOOP ( 'NONE', ( #6401, #3905, #21451, #10273 ) ) ;
#19476=DIRECTION ( 'NONE',  ( 0.000000000000000000, 0.000000000000000000, 1.000000000000000000 ) ) ;
#19480=AXIS2_PLACEMENT_3D ( 'NONE', #12484, #3800, #9218 ) ;
#19483=APPLICATION_CONTEXT ( 'automotive_design' ) ;
#19487=ADVANCED_FACE ( 'NONE', ( #6985 ), #13857, .F. ) ;
#19488=AXIS2_PLACEMENT_3D ( 'NONE', #11436, #1079, #9862 ) ;
#19490=AXIS2_PLACEMENT_3D ( 'NONE', #18246, #9688, #9359 ) ;
#19509=AXIS2_PLACEMENT_3D ( 'NONE', #4091, #2181, #9062 ) ;
#19528=CARTESIAN_POINT ( 'NONE',  ( 0.000000000000000000, 0.000000000000000000, -60.00000000000000000 ) ) ;
#19544=VERTEX_POINT ( 'NONE', #9234 ) ;
#19573=DIRECTION ( 'NONE',  ( -1.000000000000000000, 0.000000000000000000, 0.000000000000000000 ) ) ;
#19575=AXIS2_PLACEMENT_3D ( 'NONE', #18329, #7978, #2563 ) ;
#19596=AXIS2_PLACEMENT_3D ( 'NONE', #3617, #20386, #32 ) ;
#19615=CARTESIAN_POINT ( 'NONE',  ( -21.80000000000000071, 0.000000000000000000, -78.50000000000000000 ) ) ;
#19620=ORIENTED_EDGE ( 'NONE', *, *, #14219, .T. ) ;
#19634=ORIENTED_EDGE ( 'NONE', *, *, #5897, .T. ) ;
#19675=VERTEX_POINT ( 'NONE', #4255 ) ;
#19745=DIRECTION ( 'NONE',  ( 0.000000000000000000, 0.000000000000000000, 1.000000000000000000 ) ) ;
#19761=VERTEX_POINT ( 'NONE', #11355 ) ;
#19776=DIRECTION ( 'NONE',  ( 1.000000000000000000, 0.000000000000000000, -0.000000000000000000 ) ) ;
#19783=ORIENTED_EDGE ( 'NONE', *, *, #550, .F. ) ;
#19796=CARTESIAN_POINT ( 'NONE',  ( 0.000000000000000000, 25.00000000000000000, 75.00000000000000000 ) ) ;
#19803=LINE ( 'NONE', #17922, #2365 ) ;
#19810=CIRCLE ( 'NONE', #6162, 23.00000000000000000 ) ;
#19815=CIRCLE ( 'NONE', #2576, 23.00000000000000000 ) ;
#19837=DIRECTION ( 'NONE',  ( -1.000000000000000000, 0.000000000000000000, 0.000000000000000000 ) ) ;
#19846=ORIENTED_EDGE ( 'NONE', *, *, #8856, .T. ) ;
#19854=DIRECTION ( 'NONE',  ( 0.000000000000000000, 0.000000000000000000, -1.000000000000000000 ) ) ;
#19915=FACE_OUTER_BOUND ( 'NONE', #961, .T. ) ;
#19932=VERTEX_POINT ( 'NONE', #4475 ) ;
#19941=AXIS2_PLACEMENT_3D ( 'NONE', #14682, #4531, #21516 ) ;
#19959=SHAPE_DEFINITION_REPRESENTATION ( #1694, #13052 ) ;
#19973=LINE ( 'NONE', #18527, #14836 ) ;
#19977=VERTEX_POINT ( 'NONE', #1332 ) ;
#19999=CARTESIAN_POINT ( 'NONE',  ( 1.526556658859590243E-13, -21.00000000000000000, -75.00000000000000000 ) ) ;
#20022=DIRECTION ( 'NONE',  ( 0.000000000000000000, 0.000000000000000000, -1.000000000000000000 ) ) ;
#20037=CARTESIAN_POINT ( 'NONE',  ( 0.000000000000000000, 21.80000000000000071, 78.50000000000000000 ) ) ;
#20061=CARTESIAN_POINT ( 'NONE',  ( -23.00000000000000000, 0.000000000000000000, 75.00000000000000000 ) ) ;
#20089=VERTEX_POINT ( 'NONE', #11685 ) ;
#20094=LINE ( 'NONE', #14952, #7342 ) ;
#20117=EDGE_CURVE ( 'NONE', #20783, #20366, #18080, .T. ) ;
#20139=DIRECTION ( 'NONE',  ( 0.000000000000000000, 0.000000000000000000, -1.000000000000000000 ) ) ;
#20147=VERTEX_POINT ( 'NONE', #13261 ) ;
#20161=ADVANCED_FACE ( 'NONE', ( #3642 ), #4809, .T. ) ;
#20165=AXIS2_PLACEMENT_3D ( 'NONE', #9727, #5394, #18391 ) ;
#20195=ORIENTED_EDGE ( 'NONE', *, *, #14186, .F. ) ;
#20205=AXIS2_PLACEMENT_3D ( 'NONE', #7519, #14387, #21220 ) ;
#20208=CARTESIAN_POINT ( 'NONE',  ( -21.00000000000000000, 0.000000000000000000, -75.00000000000000000 ) ) ;
#20221=ORIENTED_EDGE ( 'NONE', *, *, #12275, .F. ) ;
#20238=AXIS2_PLACEMENT_3D ( 'NONE', #2315, #15952, #21212 ) ;
#20261=EDGE_LOOP ( 'NONE', ( #20446, #21247, #3706, #7810, #10073, #7850 ) ) ;
#20265=ADVANCED_FACE ( 'NONE', ( #3005 ), #13154, .F. ) ;
#20271=( LENGTH_UNIT ( ) NAMED_UNIT ( * ) SI_UNIT ( .MILLI., .METRE. ) );
#20280=DIRECTION ( 'NONE',  ( 0.000000000000000000, 0.000000000000000000, -1.000000000000000000 ) ) ;
#20308=ORIENTED_EDGE ( 'NONE', *, *, #19426, .F. ) ;
#20323=DIRECTION ( 'NONE',  ( -1.000000000000000000, 0.000000000000000000, 0.000000000000000000 ) ) ;
#20332=ORIENTED_EDGE ( 'NONE', *, *, #5326, .T. ) ;
#20366=VERTEX_POINT ( 'NONE', #9774 ) ;
#20370=DIRECTION ( 'NONE',  ( 0.000000000000000000, 0.000000000000000000, -1.000000000000000000 ) ) ;
#20384=EDGE_CURVE ( 'NONE', #19977, #21087, #21281, .T. ) ;
#20386=DIRECTION ( 'NONE',  ( 0.000000000000000000, 0.000000000000000000, -1.000000000000000000 ) ) ;
#20394=CARTESIAN_POINT ( 'NONE',  ( 0.000000000000000000, -23.00000000000000000, -75.00000000000000000 ) ) ;
#20398=EDGE_CURVE ( 'NONE', #20089, #20147, #18960, .T. ) ;
#20402=EDGE_CURVE ( 'NONE', #3651, #21555, #14490, .T. ) ;
#20424=DIRECTION ( 'NONE',  ( 0.000000000000000000, -1.000000000000000000, 0.000000000000000000 ) ) ;
#20425=EDGE_CURVE ( 'NONE', #20853, #215, #4401, .T. ) ;
#20426=VERTEX_POINT ( 'NONE', #9888 ) ;
#20431=DIRECTION ( 'NONE',  ( 0.000000000000000000, 0.000000000000000000, -1.000000000000000000 ) ) ;
#20436=CARTESIAN_POINT ( 'NONE',  ( 1.526556658859590243E-13, -22.63401512838748175, -77.51594804401857175 ) ) ;
#20446=ORIENTED_EDGE ( 'NONE', *, *, #13126, .T. ) ;
#20486=ORIENTED_EDGE ( 'NONE', *, *, #11762, .F. ) ;
#20492=AXIS2_PLACEMENT_3D ( 'NONE', #7282, #20989, #12457 ) ;
#20545=VECTOR ( 'NONE', #5791, 1000.000000000000000 ) ;
#20553=EDGE_CURVE ( 'NONE', #1152, #15384, #9388, .T. ) ;
#20573=DIRECTION ( 'NONE',  ( -1.000000000000000000, 0.000000000000000000, 0.000000000000000000 ) ) ;
#20601=ORIENTED_EDGE ( 'NONE', *, *, #21445, .T. ) ;
#20603=ADVANCED_FACE ( 'NONE', ( #3978 ), #12325, .F. ) ;
#20610=( NAMED_UNIT ( * ) PLANE_ANGLE_UNIT ( ) SI_UNIT ( $, .RADIAN. ) );
#20616=AXIS2_PLACEMENT_3D ( 'NONE', #2779, #21460, #9556 ) ;
#20632=DIRECTION ( 'NONE',  ( -1.000000000000000000, 0.000000000000000000, 0.000000000000000000 ) ) ;
#20639=CARTESIAN_POINT ( 'NONE',  ( 0.000000000000000000, 0.000000000000000000, -55.00000000000000000 ) ) ;
#20645=VERTEX_POINT ( 'NONE', #10749 ) ;
#20650=FACE_OUTER_BOUND ( 'NONE', #9647, .T. ) ;
#20654=DIRECTION ( 'NONE',  ( 0.000000000000000000, 0.000000000000000000, -1.000000000000000000 ) ) ;
#20687=CIRCLE ( 'NONE', #11006, 21.63401512838748175 ) ;
#20690=EDGE_CURVE ( 'NONE', #18856, #16533, #22021, .T. ) ;
#20692=CARTESIAN_POINT ( 'NONE',  ( 1.665334536937734811E-13, -24.63401512838747820, -77.51594804401857175 ) ) ;
#20696=CARTESIAN_POINT ( 'NONE',  ( 0.000000000000000000, -23.00000000000000000, -60.00000000000000000 ) ) ;
#20745=CARTESIAN_POINT ( 'NONE',  ( 0.000000000000000000, 19.63401512838747820, -77.51594804401857175 ) ) ;
#20772=DIRECTION ( 'NONE',  ( -1.000000000000000000, 0.000000000000000000, 0.000000000000000000 ) ) ;
#20783=VERTEX_POINT ( 'NONE', #613 ) ;
#20818=LINE ( 'NONE', #245, #10498 ) ;
#20830=CARTESIAN_POINT ( 'NONE',  ( 0.000000000000000000, -23.00000000000000000, -69.99999999999998579 ) ) ;
#20853=VERTEX_POINT ( 'NONE', #19615 ) ;
#20882=CARTESIAN_POINT ( 'NONE',  ( 0.000000000000000000, 17.50000000000000711, -30.00000000000000000 ) ) ;
#20887=EDGE_CURVE ( 'NONE', #21087, #13000, #8475, .T. ) ;
#20901=VERTEX_POINT ( 'NONE', #17838 ) ;
#20914=CARTESIAN_POINT ( 'NONE',  ( 0.000000000000000000, 0.000000000000000000, -24.99999999999999645 ) ) ;
#20953=VECTOR ( 'NONE', #10770, 1000.000000000000000 ) ;
#20969=CARTESIAN_POINT ( 'NONE',  ( 0.000000000000000000, -25.00000000000000000, 75.00000000000000000 ) ) ;
#20989=DIRECTION ( 'NONE',  ( -0.000000000000000000, -0.000000000000000000, -1.000000000000000000 ) ) ;
#20999=DIRECTION ( 'NONE',  ( 0.000000000000000000, 0.000000000000000000, -1.000000000000000000 ) ) ;
#21012=EDGE_LOOP ( 'NONE', ( #7845, #15119, #10788, #5121, #16761, #5512, #8211, #728, #5911, #6627, #15583, #8167, #435, #10808, #1019, #10343, #1783, #6769, #7035, #7769, #5430, #19325, #7657, #4404, #20332, #16293 ) ) ;
#21017=STYLED_ITEM ( 'NONE', ( #5582 ), #11503 ) ;
#21030=CARTESIAN_POINT ( 'NONE',  ( 0.000000000000000000, -17.50000000000000711, -30.00000000000000000 ) ) ;
#21053=AXIS2_PLACEMENT_3D ( 'NONE', #7127, #17248, #17359 ) ;
#21087=VERTEX_POINT ( 'NONE', #18382 ) ;
#21094=DIRECTION ( 'NONE',  ( -0.000000000000000000, -0.000000000000000000, -1.000000000000000000 ) ) ;
#21095=ORIENTED_EDGE ( 'NONE', *, *, #18214, .T. ) ;
#21106=CARTESIAN_POINT ( 'NONE',  ( 1.665334536937734811E-13, -23.00000000000000000, 69.99999999999998579 ) ) ;
#21134=CYLINDRICAL_SURFACE ( 'NONE', #13491, 17.50000000000000711 ) ;
#21161=EDGE_CURVE ( 'NONE', #13588, #20089, #211, .T. ) ;
#21163=DIRECTION ( 'NONE',  ( -1.000000000000000000, -0.000000000000000000, -0.000000000000000000 ) ) ;
#21179=EDGE_LOOP ( 'NONE', ( #17748, #14675, #11334, #3819 ) ) ;
#21199=DIRECTION ( 'NONE',  ( -1.000000000000000000, 0.000000000000000000, 0.000000000000000000 ) ) ;
#21209=VERTEX_POINT ( 'NONE', #15014 ) ;
#21212=DIRECTION ( 'NONE',  ( -1.000000000000000000, 0.000000000000000000, 0.000000000000000000 ) ) ;
#21220=DIRECTION ( 'NONE',  ( 0.000000000000000000, 0.000000000000000000, -1.000000000000000000 ) ) ;
#21238=DIRECTION ( 'NONE',  ( 0.000000000000000000, 0.000000000000000000, -1.000000000000000000 ) ) ;
#21247=ORIENTED_EDGE ( 'NONE', *, *, #9702, .T. ) ;
#21267=DIRECTION ( 'NONE',  ( -0.000000000000000000, -0.000000000000000000, -1.000000000000000000 ) ) ;
#21281=CIRCLE ( 'NONE', #6208, 3.000000000000002665 ) ;
#21304=DIRECTION ( 'NONE',  ( -1.000000000000000000, 0.000000000000000000, 0.000000000000000000 ) ) ;
#21317=AXIS2_PLACEMENT_3D ( 'NONE', #19528, #4114, #12791 ) ;
#21318=CARTESIAN_POINT ( 'NONE',  ( 0.000000000000000000, 0.000000000000000000, -60.00000000000000000 ) ) ;
#21331=ORIENTED_EDGE ( 'NONE', *, *, #20117, .T. ) ;
#21348=FACE_OUTER_BOUND ( 'NONE', #19296, .T. ) ;
#21369=EDGE_CURVE ( 'NONE', #2436, #20426, #18537, .T. ) ;
#21371=EDGE_CURVE ( 'NONE', #13588, #8719, #9611, .T. ) ;
#21379=CARTESIAN_POINT ( 'NONE',  ( 0.000000000000000000, 23.00000000000000000, -55.00000000000000711 ) ) ;
#21380=ORIENTED_EDGE ( 'NONE', *, *, #12149, .T. ) ;
#21404=EDGE_CURVE ( 'NONE', #18247, #13588, #11407, .T. ) ;
#21421=DIRECTION ( 'NONE',  ( 0.000000000000000000, 0.000000000000000000, -1.000000000000000000 ) ) ;
#21422=EDGE_LOOP ( 'NONE', ( #516, #15601, #11833, #15007 ) ) ;
#21445=EDGE_CURVE ( 'NONE', #215, #11287, #13508, .T. ) ;
#21451=ORIENTED_EDGE ( 'NONE', *, *, #9228, .T. ) ;
#21460=DIRECTION ( 'NONE',  ( -0.000000000000000000, -0.000000000000000000, -1.000000000000000000 ) ) ;
#21516=DIRECTION ( 'NONE',  ( -1.000000000000000000, 0.000000000000000000, 0.000000000000000000 ) ) ;
#21526=DIRECTION ( 'NONE',  ( -1.000000000000000000, 0.000000000000000000, 0.000000000000000000 ) ) ;
#21532=PRODUCT_CONTEXT ( 'NONE', #19483, 'mechanical' ) ;
#21540=EDGE_CURVE ( 'NONE', #17987, #3651, #14228, .T. ) ;
#21551=VERTEX_POINT ( 'NONE', #1612 ) ;
#21555=VERTEX_POINT ( 'NONE', #6791 ) ;
#21561=CYLINDRICAL_SURFACE ( 'NONE', #8344, 23.00000000000000000 ) ;
#21564=PRODUCT_DEFINITION_CONTEXT ( 'detailed design', #5686, 'design' ) ;
#21568=EDGE_CURVE ( 'NONE', #17859, #10528, #16808, .T. ) ;
#21604=DIRECTION ( 'NONE',  ( 0.000000000000000000, 0.000000000000000000, -1.000000000000000000 ) ) ;
#21611=AXIS2_PLACEMENT_3D ( 'NONE', #2632, #9513, #19837 ) ;
#21619=ORIENTED_EDGE ( 'NONE', *, *, #4856, .T. ) ;
#21622=VECTOR ( 'NONE', #9353, 1000.000000000000000 ) ;
#21638=DIRECTION ( 'NONE',  ( -1.000000000000000000, 0.000000000000000000, 0.000000000000000000 ) ) ;
#21655=MANIFOLD_SOLID_BREP ( 'Mirror2', #6121 ) ;
#21660=AXIS2_PLACEMENT_3D ( 'NONE', #12656, #5564, #7267 ) ;
#21676=CARTESIAN_POINT ( 'NONE',  ( 0.000000000000000000, 21.63401512838747820, -77.51594804401857175 ) ) ;
#21677=AXIS2_PLACEMENT_3D ( 'NONE', #20692, #4029, #3920 ) ;
#21691=CIRCLE ( 'NONE', #6972, 21.00000000000000000 ) ;
#21711=PLANE ( 'NONE',  #5473 ) ;
#21717=DIRECTION ( 'NONE',  ( -0.000000000000000000, -0.000000000000000000, -1.000000000000000000 ) ) ;
#21740=AXIS2_PLACEMENT_3D ( 'NONE', #447, #1905, #557 ) ;
#21742=AXIS2_PLACEMENT_3D ( 'NONE', #2731, #6443, #9949 ) ;
#21767=CARTESIAN_POINT ( 'NONE',  ( 0.000000000000000000, 22.63401512838748175, -77.51594804401857175 ) ) ;
#21779=ORIENTED_EDGE ( 'NONE', *, *, #20690, .T. ) ;
#21784=CARTESIAN_POINT ( 'NONE',  ( 0.000000000000000000, 0.000000000000000000, -24.99999999999999645 ) ) ;
#21785=ORIENTED_EDGE ( 'NONE', *, *, #586, .T. ) ;
#21802=CARTESIAN_POINT ( 'NONE',  ( -24.63401512838747820, 0.000000000000000000, -77.51594804401857175 ) ) ;
#21809=VERTEX_POINT ( 'NONE', #15126 ) ;
#21846=ORIENTED_EDGE ( 'NONE', *, *, #7475, .F. ) ;
#21863=DIRECTION ( 'NONE',  ( -1.000000000000000000, 0.000000000000000000, 0.000000000000000000 ) ) ;
#21882=CARTESIAN_POINT ( 'NONE',  ( 0.000000000000000000, 0.000000000000000000, -69.99999999999998579 ) ) ;
#21894=ORIENTED_EDGE ( 'NONE', *, *, #7097, .F. ) ;
#21912=CARTESIAN_POINT ( 'NONE',  ( 1.665334536937734811E-13, -24.63401512838747820, 77.51594804401857175 ) ) ;
#21965=PRESENTATION_STYLE_ASSIGNMENT (( #13430 ) ) ;
#21974=DIRECTION ( 'NONE',  ( -1.000000000000000000, 0.000000000000000000, 0.000000000000000000 ) ) ;
#22005=ORIENTED_EDGE ( 'NONE', *, *, #8163, .F. ) ;
#22010=FACE_OUTER_BOUND ( 'NONE', #10231, .T. ) ;
#22021=CIRCLE ( 'NONE', #19509, 23.00000000000000000 ) ;
#22028=DIRECTION ( 'NONE',  ( 0.000000000000000000, 0.000000000000000000, -1.000000000000000000 ) ) ;
#22036=EDGE_LOOP ( 'NONE', ( #8555, #15302, #5993, #16137 ) ) ;
#22042=CIRCLE ( 'NONE', #15594, 3.000000000000002665 ) ;
#22052=CIRCLE ( 'NONE', #12370, 21.80000000000000071 ) ;
#22066=ORIENTED_EDGE ( 'NONE', *, *, #22215, .T. ) ;
#22075=CIRCLE ( 'NONE', #152, 19.79999999999999716 ) ;
#22091=AXIS2_PLACEMENT_3D ( 'NONE', #6304, #17609, #13178 ) ;
#22097=LINE ( 'NONE', #20061, #14446 ) ;
#22109=ORIENTED_EDGE ( 'NONE', *, *, #21540, .T. ) ;
#22135=DIRECTION ( 'NONE',  ( -0.000000000000000000, -0.000000000000000000, -1.000000000000000000 ) ) ;
#22146=EDGE_CURVE ( 'NONE', #13000, #862, #13529, .T. ) ;
#22152=ORIENTED_EDGE ( 'NONE', *, *, #15077, .F. ) ;
#22159=VERTEX_POINT ( 'NONE', #4065 ) ;
#22171=CARTESIAN_POINT ( 'NONE',  ( 0.000000000000000000, -25.00000000000000000, -75.00000000000000000 ) ) ;
#22182=ORIENTED_EDGE ( 'NONE', *, *, #13528, .T. ) ;
#22187=LINE ( 'NONE', #13756, #18100 ) ;
#22209=DIRECTION ( 'NONE',  ( -1.000000000000000000, 0.000000000000000000, 0.000000000000000000 ) ) ;
#22215=EDGE_CURVE ( 'NONE', #17518, #7303, #19803, .T. ) ;
#22217=VERTEX_POINT ( 'NONE', #802 ) ;
ENDSEC;
END-ISO-10303-21;
